ISO-10303-21;
HEADER;
FILE_DESCRIPTION (('STEP AP214'),
    '1' );
FILE_NAME ('torque nut 03_iso_ISO 7042-M6-N.step',
    '2026-10-08T09:53:37',
    ( '' ),
    ( '' ),
    'SwSTEP 2.0',
    'SolidWorks 2026',
    '' );
FILE_SCHEMA (( 'AUTOMOTIVE_DESIGN' ));
ENDSEC;

DATA;
#14=CARTESIAN_POINT ( 'NONE',  ( -5.000000000000000000, 2.488344183252603870, -1.689918788536291405 ) ) ;
#16=CARTESIAN_POINT ( 'NONE',  ( 2.255011273957053586, 4.471571325851512846, -0.5083873451168745561 ) ) ;
#36=CONICAL_SURFACE ( 'NONE', #30016, 3.000000000000000000, 0.9599310885968762586 ) ;
#73=CARTESIAN_POINT ( 'NONE',  ( -5.000000000000000000, -2.886751345948134428, -2.080000000000000071 ) ) ;
#96=VECTOR ( 'NONE', #69294, 1000.000000000000000 ) ;
#182=CARTESIAN_POINT ( 'NONE',  ( 0.000000000000000000, 0.000000000000000000, 0.000000000000000000 ) ) ;
#231=CARTESIAN_POINT ( 'NONE',  ( 0.000000000000000000, 0.000000000000000000, -6.000000000000000000 ) ) ;
#320=CARTESIAN_POINT ( 'NONE',  ( 5.000000000000000000, 2.691270400161075216, -1.881368198414912429 ) ) ;
#354=CARTESIAN_POINT ( 'NONE',  ( -5.000000000000000000, -0.4878135028931876449, -6.000000000000001776 ) ) ;
#377=CARTESIAN_POINT ( 'NONE',  ( -5.000000000000000000, 1.352381405509855972, -0.8629530094790016648 ) ) ;
#379=CARTESIAN_POINT ( 'NONE',  ( 3.447886558751866115, 3.782864459065575780, -0.7348938709837807837 ) ) ;
#478=DIRECTION ( 'NONE',  ( -0.8191520442889917986, 1.003171929053524747E-16, 0.5735764363510460484 ) ) ;
#485=EDGE_CURVE ( 'NONE', #55045, #70907, #20950, .T. ) ;
#802=EDGE_CURVE ( 'NONE', #24152, #23304, #61645, .T. ) ;
#838=EDGE_CURVE ( 'NONE', #24699, #32014, #49262, .T. ) ;
#852=VERTEX_POINT ( 'NONE', #15772 ) ;
#1012=ADVANCED_FACE ( 'NONE', ( #22160 ), #34862, .T. ) ;
#1103=ORIENTED_EDGE ( 'NONE', *, *, #70883, .T. ) ;
#1152=ORIENTED_EDGE ( 'NONE', *, *, #27406, .T. ) ;
#1234=EDGE_LOOP ( 'NONE', ( #47291, #63723 ) ) ;
#1269=DIRECTION ( 'NONE',  ( -0.000000000000000000, -0.000000000000000000, 1.000000000000000000 ) ) ;
#1286=CARTESIAN_POINT ( 'NONE',  ( -5.000000000000000000, 2.419979747126332903, -5.688163366729713566 ) ) ;
#1374=FACE_OUTER_BOUND ( 'NONE', #64661, .T. ) ;
#1436=EDGE_LOOP ( 'NONE', ( #22950, #70821, #30835 ) ) ;
#1518=ORIENTED_EDGE ( 'NONE', *, *, #22646, .F. ) ;
#1536=CARTESIAN_POINT ( 'NONE',  ( 4.999999999999999112, -0.2835658343809315252, -0.5205273423269578537 ) ) ;
#1556=CARTESIAN_POINT ( 'NONE',  ( 6.078523336270777024E-16, 5.773502691896261751, -6.000000000000000000 ) ) ;
#1590=CARTESIAN_POINT ( 'NONE',  ( 3.000000000000000000, 0.000000000000000000, -6.000000000000001776 ) ) ;
#1735=DIRECTION ( 'NONE',  ( 1.000000000000000000, 0.000000000000000000, 0.000000000000000000 ) ) ;
#1740=CARTESIAN_POINT ( 'NONE',  ( 1.301042606982605321E-15, 5.773502691896264416, -5.553418012614792509 ) ) ;
#1829=CARTESIAN_POINT ( 'NONE',  ( 5.000000000000000888, 0.9828435001097636237, -5.956909652965543422 ) ) ;
#1861=AXIS2_PLACEMENT_3D ( 'NONE', #8469, #42316, #64498 ) ;
#1957=LINE ( 'NONE', #24475, #11872 ) ;
#1999=DIRECTION ( 'NONE',  ( 0.000000000000000000, -0.000000000000000000, 1.000000000000000000 ) ) ;
#2017=EDGE_CURVE ( 'NONE', #24699, #18969, #8786, .T. ) ;
#2103=CYLINDRICAL_SURFACE ( 'NONE', #73824, 2.500000000000000000 ) ;
#2276=DIRECTION ( 'NONE',  ( 1.000000000000000000, 0.000000000000000000, 0.000000000000000000 ) ) ;
#2296=DIRECTION ( 'NONE',  ( 1.000000000000000000, 0.000000000000000000, 0.000000000000000000 ) ) ;
#2297=CARTESIAN_POINT ( 'NONE',  ( 0.000000000000000000, 5.773502691896262640, 0.000000000000000000 ) ) ;
#2308=DIRECTION ( 'NONE',  ( 0.000000000000000000, 0.000000000000000000, 1.000000000000000000 ) ) ;
#2334=AXIS2_PLACEMENT_3D ( 'NONE', #66121, #42441, #70988 ) ;
#2494=DIRECTION ( 'NONE',  ( -0.000000000000000000, -0.000000000000000000, 1.000000000000000000 ) ) ;
#2574=CARTESIAN_POINT ( 'NONE',  ( -2.500000000000003997, 4.330127018922192761, -6.000000000000000000 ) ) ;
#2617=VERTEX_POINT ( 'NONE', #38632 ) ;
#2638=ORIENTED_EDGE ( 'NONE', *, *, #47490, .F. ) ;
#2662=CARTESIAN_POINT ( 'NONE',  ( 0.000000000000000000, 0.000000000000000000, 0.000000000000000000 ) ) ;
#2711=ORIENTED_EDGE ( 'NONE', *, *, #39044, .F. ) ;
#2747=AXIS2_PLACEMENT_3D ( 'NONE', #4317, #55800, #50893 ) ;
#2857=AXIS2_PLACEMENT_3D ( 'NONE', #9383, #49598, #19912 ) ;
#2926=CARTESIAN_POINT ( 'NONE',  ( 2.500000000000003109, -4.330127018922192761, -6.000000000000000000 ) ) ;
#2967=DIRECTION ( 'NONE',  ( -0.8191520442889890230, 0.000000000000000000, -0.5735764363510501562 ) ) ;
#3041=CARTESIAN_POINT ( 'NONE',  ( -2.503857664561936813E-16, -5.773502691896267081, -6.000000000000000000 ) ) ;
#3088=ORIENTED_EDGE ( 'NONE', *, *, #35130, .F. ) ;
#3213=CARTESIAN_POINT ( 'NONE',  ( 0.000000000000000000, 0.000000000000000000, -6.000000000000000000 ) ) ;
#3249=EDGE_CURVE ( 'NONE', #46616, #36077, #39445, .T. ) ;
#3312=CARTESIAN_POINT ( 'NONE',  ( -1.648146632869002426, -4.821944789745372439, -6.000000000000000000 ) ) ;
#3355=DIRECTION ( 'NONE',  ( 0.8191520442889890230, 1.003171929053521295E-16, -0.5735764363510501562 ) ) ;
#3458=ORIENTED_EDGE ( 'NONE', *, *, #49891, .F. ) ;
#3464=ORIENTED_EDGE ( 'NONE', *, *, #9569, .F. ) ;
#3494=CARTESIAN_POINT ( 'NONE',  ( -2.018853055115723105, 4.607917337070899677, -0.5666985376598566715 ) ) ;
#3541=ORIENTED_EDGE ( 'NONE', *, *, #14309, .F. ) ;
#3666=AXIS2_PLACEMENT_3D ( 'NONE', #36154, #52331, #24505 ) ;
#3895=VERTEX_POINT ( 'NONE', #16674 ) ;
#3920=FACE_OUTER_BOUND ( 'NONE', #21453, .T. ) ;
#3979=ORIENTED_EDGE ( 'NONE', *, *, #4510, .T. ) ;
#4208=CARTESIAN_POINT ( 'NONE',  ( 0.7207917504152147048, -5.357353380764381612, -1.325189086772950331 ) ) ;
#4231=CARTESIAN_POINT ( 'NONE',  ( -1.332830945733270545, 5.003992386592893915, -0.8603634151101617888 ) ) ;
#4273=EDGE_CURVE ( 'NONE', #54553, #47718, #20355, .T. ) ;
#4275=CARTESIAN_POINT ( 'NONE',  ( 6.078523336270777024E-16, 5.773502691896261751, -6.000000000000000000 ) ) ;
#4317=CARTESIAN_POINT ( 'NONE',  ( 0.000000000000000000, 0.000000000000000000, -0.3851141460153411078 ) ) ;
#4510=EDGE_CURVE ( 'NONE', #33146, #2617, #36823, .T. ) ;
#4542=CARTESIAN_POINT ( 'NONE',  ( 1.301042606982605321E-15, 5.773502691896264416, -5.553418012614792509 ) ) ;
#4579=CARTESIAN_POINT ( 'NONE',  ( 2.381231458764692110, -4.398698068175666442, -0.5078976954043025183 ) ) ;
#4656=CONICAL_SURFACE ( 'NONE', #25025, 5.000000000000000888, 1.047197551196596299 ) ;
#4723=EDGE_LOOP ( 'NONE', ( #17058, #45039, #72051 ) ) ;
#4787=FACE_BOUND ( 'NONE', #26242, .T. ) ;
#4969=DIRECTION ( 'NONE',  ( 1.000000000000000000, 0.000000000000000000, 0.000000000000000000 ) ) ;
#5200=AXIS2_PLACEMENT_3D ( 'NONE', #59692, #60805, #31476 ) ;
#5212=ORIENTED_EDGE ( 'NONE', *, *, #27406, .F. ) ;
#5347=CARTESIAN_POINT ( 'NONE',  ( -0.7207917504152121513, 5.357353380764376283, -1.325189086772940117 ) ) ;
#5476=DIRECTION ( 'NONE',  ( 0.5000000000000009992, 0.8660254037844381525, -0.000000000000000000 ) ) ;
#5668=CARTESIAN_POINT ( 'NONE',  ( 5.000000000000000000, -0.6964580643377611402, -0.6026403643956901313 ) ) ;
#5712=CARTESIAN_POINT ( 'NONE',  ( -5.000000000000000000, 2.886751345948126879, -6.000000000000000000 ) ) ;
#5839=ORIENTED_EDGE ( 'NONE', *, *, #60838, .T. ) ;
#6032=EDGE_LOOP ( 'NONE', ( #37727, #11218, #1518, #21287, #50002 ) ) ;
#6043=CARTESIAN_POINT ( 'NONE',  ( 5.000000000000000000, -2.058885705017528878, -1.328630925609301183 ) ) ;
#6140=CARTESIAN_POINT ( 'NONE',  ( 3.000000000000000000, 3.673940397442059868E-16, -5.974599999999999689 ) ) ;
#6458=ADVANCED_FACE ( 'NONE', ( #65341 ), #37511, .F. ) ;
#6536=CARTESIAN_POINT ( 'NONE',  ( 3.000000000000000000, 0.000000000000000000, 0.000000000000000000 ) ) ;
#6578=ORIENTED_EDGE ( 'NONE', *, *, #53204, .T. ) ;
#6608=CARTESIAN_POINT ( 'NONE',  ( -3.447886558751868336, -3.782864459065579776, -0.7348938709837913308 ) ) ;
#6817=ORIENTED_EDGE ( 'NONE', *, *, #10021, .T. ) ;
#6859=DIRECTION ( 'NONE',  ( -1.000000000000000000, 0.000000000000000000, 0.000000000000000000 ) ) ;
#6959=CARTESIAN_POINT ( 'NONE',  ( 1.648146632868999539, 4.821944789745367110, -6.000000000000003553 ) ) ;
#6968=CARTESIAN_POINT ( 'NONE',  ( -2.008727693139930270, -4.613763217533273675, -0.5592653008974395323 ) ) ;
#7012=CARTESIAN_POINT ( 'NONE',  ( 4.999999999999999112, 0.2838785441256751474, -0.5080592402122395823 ) ) ;
#7135=CARTESIAN_POINT ( 'NONE',  ( 5.000000000000000000, -1.096207231254244352, -0.7463930790433302986 ) ) ;
#7166=( LENGTH_UNIT ( ) NAMED_UNIT ( * ) SI_UNIT ( .MILLI., .METRE. ) );
#7306=DIRECTION ( 'NONE',  ( -1.000000000000000000, 3.552713678800500929E-15, 0.000000000000000000 ) ) ;
#7347=CARTESIAN_POINT ( 'NONE',  ( 1.301042606982605321E-15, 5.773502691896264416, -5.553418012614792509 ) ) ;
#7612=DIRECTION ( 'NONE',  ( 0.8191520442889917986, 0.000000000000000000, 0.5735764363510460484 ) ) ;
#7706=CARTESIAN_POINT ( 'NONE',  ( -2.074714256722481664, 4.575665857285980742, -5.989444439476608650 ) ) ;
#8089=PLANE ( 'NONE',  #1861 ) ;
#8293=CIRCLE ( 'NONE', #26260, 3.000000000000000000 ) ;
#8357=B_SPLINE_CURVE_WITH_KNOTS ( 'NONE', 3,
 ( #73987, #45819, #68742, #18327, #354, #23245 ),
 .UNSPECIFIED., .F., .F.,
 ( 4, 2, 4 ),
 ( 0.005150343764683549923, 0.006610526168996381374, 0.008070708573309213693 ),
 .UNSPECIFIED. ) ;
#8469=CARTESIAN_POINT ( 'NONE',  ( -2.503857664561936813E-16, -5.773502691896267081, -6.000000000000000000 ) ) ;
#8644=FILL_AREA_STYLE_COLOUR ( '', #24135 ) ;
#8786=B_SPLINE_CURVE_WITH_KNOTS ( 'NONE', 3,
 ( #42882, #59425, #18816, #64334, #58685, #24835 ),
 .UNSPECIFIED., .F., .F.,
 ( 4, 2, 4 ),
 ( 0.005150343764683553392, 0.006610526168996383109, 0.008070708573309213693 ),
 .UNSPECIFIED. ) ;
#8797=DIRECTION ( 'NONE',  ( -1.000000000000000000, 0.000000000000000000, 0.000000000000000000 ) ) ;
#9129=VECTOR ( 'NONE', #7612, 1000.000000000000227 ) ;
#9273=EDGE_CURVE ( 'NONE', #39865, #32014, #13270, .T. ) ;
#9294=AXIS2_PLACEMENT_3D ( 'NONE', #36073, #53733, #2276 ) ;
#9383=CARTESIAN_POINT ( 'NONE',  ( 0.000000000000000000, 0.000000000000000000, 0.000000000000000000 ) ) ;
#9434=CARTESIAN_POINT ( 'NONE',  ( -4.180704885107413560, -3.359771601077115921, -5.801655677627839403 ) ) ;
#9476=CARTESIAN_POINT ( 'NONE',  ( -1.552113441248129000, 4.877389578778817736, -0.7348938709837885552 ) ) ;
#9505=AXIS2_PLACEMENT_3D ( 'NONE', #231, #18207, #7306 ) ;
#9514=VECTOR ( 'NONE', #56766, 1000.000000000000000 ) ;
#9569=EDGE_CURVE ( 'NONE', #18028, #36601, #40666, .T. ) ;
#9694=FACE_OUTER_BOUND ( 'NONE', #31175, .T. ) ;
#9936=COLOUR_RGB ( '', 0.09019608, 0.27058824, 0.51372549) ;
#10021=EDGE_CURVE ( 'NONE', #69466, #55663, #8293, .T. ) ;
#10140=CARTESIAN_POINT ( 'NONE',  ( -2.500000000000000000, 3.061616997868383141E-16, -6.000000000000000000 ) ) ;
#10284=EDGE_LOOP ( 'NONE', ( #48432, #38739, #46367, #2711, #52690, #21077 ) ) ;
#10356=( NAMED_UNIT ( * ) PLANE_ANGLE_UNIT ( ) SI_UNIT ( $, .RADIAN. ) );
#10366=CARTESIAN_POINT ( 'NONE',  ( -2.500000000000000000, 3.061616997868383141E-16, -0.3501037691048548561 ) ) ;
#10516=LINE ( 'NONE', #17652, #50965 ) ;
#10561=CARTESIAN_POINT ( 'NONE',  ( 1.332830945733272987, -5.003992386592898356, -0.8603634151101718919 ) ) ;
#10582=PLANE ( 'NONE',  #33410 ) ;
#10630=B_SPLINE_CURVE_WITH_KNOTS ( 'NONE', 3,
 ( #18246, #63760, #7706, #53201, #24992, #70107, #52447, #1740 ),
 .UNSPECIFIED., .F., .F.,
 ( 4, 2, 2, 4 ),
 ( 0.002921158011986710323, 0.003648658599403066614, 0.004376159186819422904, 0.005831160361652134617 ),
 .UNSPECIFIED. ) ;
#10645=FACE_OUTER_BOUND ( 'NONE', #46091, .T. ) ;
#10828=DIRECTION ( 'NONE',  ( -0.000000000000000000, -0.000000000000000000, 1.000000000000000000 ) ) ;
#10942=EDGE_CURVE ( 'NONE', #18969, #852, #51863, .T. ) ;
#11011=ORIENTED_EDGE ( 'NONE', *, *, #35130, .T. ) ;
#11056=DIRECTION ( 'NONE',  ( 1.000000000000000000, 0.000000000000000000, 0.000000000000000000 ) ) ;
#11094=FACE_OUTER_BOUND ( 'NONE', #35940, .T. ) ;
#11218=ORIENTED_EDGE ( 'NONE', *, *, #4273, .T. ) ;
#11276=DIRECTION ( 'NONE',  ( -0.000000000000000000, -0.000000000000000000, 1.000000000000000000 ) ) ;
#11398=CARTESIAN_POINT ( 'NONE',  ( -5.000000000000000000, 0.000000000000000000, -6.000000000000000000 ) ) ;
#11496=CARTESIAN_POINT ( 'NONE',  ( -2.739742549670663330, -4.191711593333635300, -0.5197061503823270368 ) ) ;
#11592=CARTESIAN_POINT ( 'NONE',  ( -4.999999999999999112, 1.831554690317574341, -1.158389257021580576 ) ) ;
#11594=CARTESIAN_POINT ( 'NONE',  ( 3.101151694651712809, 3.983051926191225611, -0.6020238742160355372 ) ) ;
#11785=MANIFOLD_SOLID_BREP ( 'EndChamfer', #46382 ) ;
#11872=VECTOR ( 'NONE', #478, 1000.000000000000227 ) ;
#12005=ORIENTED_EDGE ( 'NONE', *, *, #25310, .F. ) ;
#12015=DIRECTION ( 'NONE',  ( 1.000000000000000000, 0.000000000000000000, 0.000000000000000000 ) ) ;
#12031=CARTESIAN_POINT ( 'NONE',  ( -5.000000000000000000, -0.9645339558193164464, -0.6919071587033235327 ) ) ;
#12050=CARTESIAN_POINT ( 'NONE',  ( 0.000000000000000000, 0.000000000000000000, -5.624496230895140947 ) ) ;
#12171=DIRECTION ( 'NONE',  ( 0.4415113423096792000, 5.406954521468000113E-17, -0.8972556684757725387 ) ) ;
#12239=CARTESIAN_POINT ( 'NONE',  ( -2.981146944884250694, -4.052336700773510714, -0.5666985376598571156 ) ) ;
#12347=DIRECTION ( 'NONE',  ( -0.000000000000000000, -0.000000000000000000, 1.000000000000000000 ) ) ;
#12606=CARTESIAN_POINT ( 'NONE',  ( -4.828573329308746942, -2.985724580418009921, -1.878862934774787830 ) ) ;
#13059=CARTESIAN_POINT ( 'NONE',  ( 5.000000000000000000, 2.419979747126332903, -5.688163366729713566 ) ) ;
#13118=CIRCLE ( 'NONE', #2334, 4.749999999999999112 ) ;
#13270=CIRCLE ( 'NONE', #33658, 5.000000000000000888 ) ;
#13340=CIRCLE ( 'NONE', #22965, 2.500000000000000000 ) ;
#13442=ORIENTED_EDGE ( 'NONE', *, *, #58136, .T. ) ;
#13478=ORIENTED_EDGE ( 'NONE', *, *, #49318, .T. ) ;
#13482=CIRCLE ( 'NONE', #55519, 3.000000000000000000 ) ;
#13487=EDGE_CURVE ( 'NONE', #65774, #17672, #15514, .T. ) ;
#13711=FACE_OUTER_BOUND ( 'NONE', #1436, .T. ) ;
#13774=VERTEX_POINT ( 'NONE', #32802 ) ;
#13824=CARTESIAN_POINT ( 'NONE',  ( -3.000000000000000000, 0.000000000000000000, -5.974599999999999689 ) ) ;
#13884=DIRECTION ( 'NONE',  ( 0.000000000000000000, 0.000000000000000000, 1.000000000000000000 ) ) ;
#14048=CARTESIAN_POINT ( 'NONE',  ( 4.749999999999999112, 6.447547231611302361E-16, 0.000000000000000000 ) ) ;
#14275=CIRCLE ( 'NONE', #25122, 3.000000000000000000 ) ;
#14309=EDGE_CURVE ( 'NONE', #39865, #45184, #14792, .T. ) ;
#14474=UNCERTAINTY_MEASURE_WITH_UNIT (LENGTH_MEASURE( 1.000000000000000082E-05 ), #49830, 'distance_accuracy_value', 'NONE');
#14535=ORIENTED_EDGE ( 'NONE', *, *, #2017, .F. ) ;
#14580=ADVANCED_FACE ( 'NONE', ( #36807 ), #68121, .T. ) ;
#14595=B_SPLINE_CURVE_WITH_KNOTS ( 'NONE', 3,
 ( #2926, #18688, #43132, #42013, #48380, #70549, #60058, #59297 ),
 .UNSPECIFIED., .F., .F.,
 ( 4, 2, 2, 4 ),
 ( 0.002921158011986708155, 0.003648658599403065313, 0.004376159186819422037, 0.005831160361652136352 ),
 .UNSPECIFIED. ) ;
#14650=CARTESIAN_POINT ( 'NONE',  ( 2.500000000000003109, -4.330127018922192761, -6.000000000000000000 ) ) ;
#14785=EDGE_CURVE ( 'NONE', #45184, #17672, #8357, .T. ) ;
#14792=B_SPLINE_CURVE_WITH_KNOTS ( 'NONE', 3,
 ( #33467, #44777, #38010, #60943, #44403, #9434, #44029, #27458 ),
 .UNSPECIFIED., .F., .F.,
 ( 4, 2, 2, 4 ),
 ( 0.002921158011986722466, 0.003648658599403074854, 0.004376159186819426374, 0.005831160361652130281 ),
 .UNSPECIFIED. ) ;
#14883=EDGE_CURVE ( 'NONE', #32014, #45965, #14595, .T. ) ;
#15086=CARTESIAN_POINT ( 'NONE',  ( 4.652319770550017886, -3.087484620012992398, -1.687189089856322655 ) ) ;
#15121=EDGE_CURVE ( 'NONE', #55663, #69466, #13482, .T. ) ;
#15453=ORIENTED_EDGE ( 'NONE', *, *, #41198, .F. ) ;
#15514=CIRCLE ( 'NONE', #9505, 5.000000000000000888 ) ;
#15772=CARTESIAN_POINT ( 'NONE',  ( 5.000000000000000000, 2.886751345948137981, -5.553418012614792509 ) ) ;
#15892=ADVANCED_FACE ( 'NONE', ( #11094 ), #56600, .T. ) ;
#15895=ORIENTED_EDGE ( 'NONE', *, *, #4510, .F. ) ;
#15990=PRODUCT_DEFINITION_FORMATION_WITH_SPECIFIED_SOURCE ( 'ANY', '', #55381, .NOT_KNOWN. ) ;
#16138=CARTESIAN_POINT ( 'NONE',  ( -4.999999999999999112, 0.5616961504262225624, -0.5576671450146215570 ) ) ;
#16161=ORIENTED_EDGE ( 'NONE', *, *, #41198, .T. ) ;
#16206=CARTESIAN_POINT ( 'NONE',  ( 1.552113441248130554, -4.877389578778822177, -0.7348938709837993244 ) ) ;
#16348=ORIENTED_EDGE ( 'NONE', *, *, #56947, .F. ) ;
#16372=ADVANCED_FACE ( 'NONE', ( #45512 ), #19649, .T. ) ;
#16561=CARTESIAN_POINT ( 'NONE',  ( -4.999999999999999112, -1.831125658499874964, -1.158123955083390388 ) ) ;
#16657=SHAPE_DEFINITION_REPRESENTATION ( #25942, #23018 ) ;
#16674=CARTESIAN_POINT ( 'NONE',  ( -2.500000000000000000, 3.061616997868383141E-16, -5.624496230895140947 ) ) ;
#16842=EDGE_CURVE ( 'NONE', #26720, #852, #63756, .T. ) ;
#16844=CARTESIAN_POINT ( 'NONE',  ( 3.346878500200757944, 3.841181488860379911, -5.948595712916174172 ) ) ;
#16896=MECHANICAL_DESIGN_GEOMETRIC_PRESENTATION_REPRESENTATION('',(#55299),#52949);
#16915=ADVANCED_FACE ( 'NONE', ( #62345 ), #32890, .T. ) ;
#17058=ORIENTED_EDGE ( 'NONE', *, *, #14883, .T. ) ;
#17116=PRESENTATION_STYLE_ASSIGNMENT (( #61874 ) ) ;
#17257=CARTESIAN_POINT ( 'NONE',  ( 2.618768541235299896, 4.261555969668734178, -0.5078976954042870862 ) ) ;
#17308=CARTESIAN_POINT ( 'NONE',  ( -5.000000000000000000, -0.6964580643377609181, -0.6026403643956899092 ) ) ;
#17557=CARTESIAN_POINT ( 'NONE',  ( 5.000000000000000888, 0.5616961504262232285, -0.5576671450146228892 ) ) ;
#17570=DIRECTION ( 'NONE',  ( 1.000000000000000000, 0.000000000000000000, 0.000000000000000000 ) ) ;
#17642=CARTESIAN_POINT ( 'NONE',  ( 2.500000000000005773, 4.330127018922191873, -6.000000000000000000 ) ) ;
#17652=CARTESIAN_POINT ( 'NONE',  ( 2.500000000000000000, 0.000000000000000000, -6.000000000000000000 ) ) ;
#17672=VERTEX_POINT ( 'NONE', #55397 ) ;
#17680=AXIS2_PLACEMENT_3D ( 'NONE', #2297, #59041, #24813 ) ;
#18028=VERTEX_POINT ( 'NONE', #65494 ) ;
#18137=CYLINDRICAL_SURFACE ( 'NONE', #31775, 3.000000000000000000 ) ;
#18207=DIRECTION ( 'NONE',  ( 0.000000000000000000, -0.000000000000000000, 1.000000000000000000 ) ) ;
#18246=CARTESIAN_POINT ( 'NONE',  ( -2.500000000000003997, 4.330127018922192761, -6.000000000000000000 ) ) ;
#18327=CARTESIAN_POINT ( 'NONE',  ( -5.000000000000000000, -0.9724665692850904541, -5.958069561147902427 ) ) ;
#18657=CARTESIAN_POINT ( 'NONE',  ( 5.000000000000000000, 1.831554690317580780, -1.158389257021584795 ) ) ;
#18664=EDGE_LOOP ( 'NONE', ( #55512, #45638, #37758, #22366, #22130, #37936, #31456 ) ) ;
#18688=CARTESIAN_POINT ( 'NONE',  ( 2.287832656137188447, -4.452621892014642313, -5.999999999999999112 ) ) ;
#18764=ADVANCED_FACE ( 'NONE', ( #1374 ), #2103, .F. ) ;
#18783=ORIENTED_EDGE ( 'NONE', *, *, #13487, .F. ) ;
#18786=ORIENTED_EDGE ( 'NONE', *, *, #23005, .T. ) ;
#18816=CARTESIAN_POINT ( 'NONE',  ( 5.000000000000000888, -1.936377641173859798, -5.802630826755080129 ) ) ;
#18969=VERTEX_POINT ( 'NONE', #25730 ) ;
#18991=DIRECTION ( 'NONE',  ( -1.000000000000000000, 0.000000000000000000, 0.000000000000000000 ) ) ;
#19369=DIRECTION ( 'NONE',  ( 0.000000000000000000, -0.000000000000000000, 1.000000000000000000 ) ) ;
#19446=EDGE_CURVE ( 'NONE', #26473, #70907, #10516, .T. ) ;
#19461=CARTESIAN_POINT ( 'NONE',  ( 4.828573329308747830, 2.985724580418001928, -1.878862934774779836 ) ) ;
#19516=ORIENTED_EDGE ( 'NONE', *, *, #49318, .F. ) ;
#19649=CONICAL_SURFACE ( 'NONE', #28078, 5.000000000000000888, 1.047197551196596299 ) ;
#19735=DIRECTION ( 'NONE',  ( 1.000000000000000000, 0.000000000000000000, 0.000000000000000000 ) ) ;
#19912=DIRECTION ( 'NONE',  ( 1.000000000000000000, 0.000000000000000000, 0.000000000000000000 ) ) ;
#20100=VECTOR ( 'NONE', #42805, 1000.000000000000000 ) ;
#20355=B_SPLINE_CURVE_WITH_KNOTS ( 'NONE', 3,
 ( #44421, #67342, #15086, #45163, #73339, #27478, #33114, #56062, #60959, #4579, #39523, #33872, #55691, #16206, #10561, #72588, #4208, #27099, #50031, #32375 ),
 .UNSPECIFIED., .F., .F.,
 ( 4, 2, 2, 2, 2, 2, 2, 2, 2, 4 ),
 ( 2.781148944256651962E-07, 0.0008372784139787452749, 0.001674278713063064939, 0.002511279012147384603, 0.003348279311231704483, 0.003766779460773864857, 0.004185279610316025231, 0.005022279909400345112, 0.005859280208484664992, 0.006696280507568985740 ),
 .UNSPECIFIED. ) ;
#20399=CARTESIAN_POINT ( 'NONE',  ( -2.991272306860052410, 4.046490820311134939, -0.5592653008974223239 ) ) ;
#20606=DIRECTION ( 'NONE',  ( 0.8660254037844382635, -0.5000000000000006661, 0.000000000000000000 ) ) ;
#20742=LINE ( 'NONE', #48213, #43262 ) ;
#20950=CIRCLE ( 'NONE', #42595, 2.500000000000000000 ) ;
#21077=ORIENTED_EDGE ( 'NONE', *, *, #14785, .F. ) ;
#21169=DIRECTION ( 'NONE',  ( -1.000000000000000000, 0.000000000000000000, 0.000000000000000000 ) ) ;
#21254=CARTESIAN_POINT ( 'NONE',  ( 5.000000000000000000, 2.886751345948125991, -6.000000000000000000 ) ) ;
#21287=ORIENTED_EDGE ( 'NONE', *, *, #14883, .F. ) ;
#21299=AXIS2_PLACEMENT_3D ( 'NONE', #60431, #61911, #60797 ) ;
#21453=EDGE_LOOP ( 'NONE', ( #12005, #40661, #13442, #48156 ) ) ;
#21564=CARTESIAN_POINT ( 'NONE',  ( 0.000000000000000000, 0.000000000000000000, -25.03750572909317285 ) ) ;
#21717=ADVANCED_FACE ( 'NONE', ( #13711 ), #51913, .T. ) ;
#21765=ADVANCED_FACE ( 'NONE', ( #45274 ), #35117, .F. ) ;
#21915=FACE_OUTER_BOUND ( 'NONE', #31687, .T. ) ;
#22003=FACE_OUTER_BOUND ( 'NONE', #47334, .T. ) ;
#22130=ORIENTED_EDGE ( 'NONE', *, *, #69699, .F. ) ;
#22156=CARTESIAN_POINT ( 'NONE',  ( 3.035766082959412415E-15, 5.773502691896260863, -2.080000000000000071 ) ) ;
#22160=FACE_OUTER_BOUND ( 'NONE', #18664, .T. ) ;
#22172=LINE ( 'NONE', #10140, #34201 ) ;
#22249=CARTESIAN_POINT ( 'NONE',  ( 3.035766082959412415E-15, 5.773502691896260863, -2.080000000000000071 ) ) ;
#22319=CYLINDRICAL_SURFACE ( 'NONE', #32598, 3.000000000000000000 ) ;
#22366=ORIENTED_EDGE ( 'NONE', *, *, #29206, .F. ) ;
#22377=DIRECTION ( 'NONE',  ( -0.000000000000000000, -0.000000000000000000, 1.000000000000000000 ) ) ;
#22528=CARTESIAN_POINT ( 'NONE',  ( -5.000000000000000000, -4.846777557549235459E-18, -0.5080592402122449114 ) ) ;
#22620=CARTESIAN_POINT ( 'NONE',  ( -4.182066831946699814, 3.358985280702823761, -5.826062401966626503 ) ) ;
#22646=EDGE_CURVE ( 'NONE', #45965, #47718, #53401, .T. ) ;
#22648=ORIENTED_EDGE ( 'NONE', *, *, #14785, .T. ) ;
#22676=CARTESIAN_POINT ( 'NONE',  ( 0.000000000000000000, 0.000000000000000000, -25.03750572909317285 ) ) ;
#22950=ORIENTED_EDGE ( 'NONE', *, *, #56947, .T. ) ;
#22965=AXIS2_PLACEMENT_3D ( 'NONE', #70105, #58105, #24266 ) ;
#22966=CARTESIAN_POINT ( 'NONE',  ( -5.000000000000000000, -1.349638343847294752, -0.8687551798607462405 ) ) ;
#23005=EDGE_CURVE ( 'NONE', #17672, #39865, #27865, .T. ) ;
#23018=SHAPE_REPRESENTATION ( 'torque nut 03_iso_ISO 7042-M6-N', ( #43395 ), #47140 ) ;
#23069=CARTESIAN_POINT ( 'NONE',  ( -4.999999999999999112, 0.4881033300985041512, -6.000000000000000000 ) ) ;
#23159=STYLED_ITEM ( 'NONE', ( #17116 ), #74006 ) ;
#23228=CARTESIAN_POINT ( 'NONE',  ( 4.592054218142288313, 3.122278952918447814, -5.689399939901071512 ) ) ;
#23245=CARTESIAN_POINT ( 'NONE',  ( -5.000000000000000000, 0.000000000000000000, -6.000000000000000000 ) ) ;
#23304=VERTEX_POINT ( 'NONE', #14048 ) ;
#23326=CARTESIAN_POINT ( 'NONE',  ( -5.000000000000000000, -0.5603747650654237189, -0.5678343202077608121 ) ) ;
#23346=DIRECTION ( 'NONE',  ( -1.000000000000000000, 0.000000000000000000, 0.000000000000000000 ) ) ;
#23406=ORIENTED_EDGE ( 'NONE', *, *, #41832, .F. ) ;
#23525=CARTESIAN_POINT ( 'NONE',  ( -4.651285141664999401, -3.088081963278269004, -1.686035282245272215 ) ) ;
#23589=EDGE_LOOP ( 'NONE', ( #35973, #18783, #61295, #19516, #40630, #31363 ) ) ;
#23704=DIRECTION ( 'NONE',  ( -1.000000000000000000, 0.000000000000000000, 0.000000000000000000 ) ) ;
#23767=B_SPLINE_CURVE_WITH_KNOTS ( 'NONE', 3,
 ( #22528, #68398, #16138, #51455, #377, #11592, #57480, #14, #63139, #46202 ),
 .UNSPECIFIED., .F., .F.,
 ( 4, 2, 2, 2, 4 ),
 ( 0.01815567983891738443, 0.01899359644517026671, 0.01983151305142314552, 0.02066942965767602780, 0.02150734626392890661 ),
 .UNSPECIFIED. ) ;
#23798=CARTESIAN_POINT ( 'NONE',  ( 5.000000000000000000, -2.886751345948134428, -6.000000000000000000 ) ) ;
#23829=LINE ( 'NONE', #63698, #37452 ) ;
#23899=CARTESIAN_POINT ( 'NONE',  ( -1.546821644788046735, -4.880444798889548963, -0.7375898304884659362 ) ) ;
#24016=LINE ( 'NONE', #40940, #45781 ) ;
#24096=SURFACE_SIDE_STYLE ('',( #59780 ) ) ;
#24135=COLOUR_RGB ( '', 0.09019608, 0.27058824, 0.51372549) ;
#24152=VERTEX_POINT ( 'NONE', #73952 ) ;
#24264=DIRECTION ( 'NONE',  ( 0.000000000000000000, 0.000000000000000000, 1.000000000000000000 ) ) ;
#24266=DIRECTION ( 'NONE',  ( -1.000000000000000000, 0.000000000000000000, 0.000000000000000000 ) ) ;
#24271=EDGE_CURVE ( 'NONE', #47528, #40220, #54795, .T. ) ;
#24274=CARTESIAN_POINT ( 'NONE',  ( -5.000000000000000000, -2.886751345948134428, -2.080000000000000071 ) ) ;
#24316=CARTESIAN_POINT ( 'NONE',  ( 5.000000000000000000, 2.488344183252611419, -1.689918788536298289 ) ) ;
#24418=CARTESIAN_POINT ( 'NONE',  ( 4.999999999999999112, -0.1416384297035287454, -0.5080592402122392492 ) ) ;
#24475=CARTESIAN_POINT ( 'NONE',  ( -2.449999999999998845, 3.000384657911014384E-16, -0.3851141460153411078 ) ) ;
#24484=ORIENTED_EDGE ( 'NONE', *, *, #27426, .T. ) ;
#24503=CARTESIAN_POINT ( 'NONE',  ( 0.000000000000000000, 0.000000000000000000, -5.974599999999999689 ) ) ;
#24505=DIRECTION ( 'NONE',  ( -1.000000000000000000, -1.776356839400250465E-15, 0.000000000000000000 ) ) ;
#24615=ORIENTED_EDGE ( 'NONE', *, *, #19446, .F. ) ;
#24622=CARTESIAN_POINT ( 'NONE',  ( 0.000000000000000000, 0.000000000000000000, -6.000000000000000000 ) ) ;
#24699=VERTEX_POINT ( 'NONE', #69979 ) ;
#24813=DIRECTION ( 'NONE',  ( -1.000000000000000000, 0.000000000000000000, 0.000000000000000000 ) ) ;
#24835=CARTESIAN_POINT ( 'NONE',  ( 5.000000000000000888, 0.000000000000000000, -6.000000000000000000 ) ) ;
#24992=CARTESIAN_POINT ( 'NONE',  ( -1.443735181952766622, 4.939961795957295898, -5.918341802876230240 ) ) ;
#25025=AXIS2_PLACEMENT_3D ( 'NONE', #50048, #26393, #4969 ) ;
#25109=CARTESIAN_POINT ( 'NONE',  ( 4.651285141665000289, 3.088081963278261011, -1.686035282245264444 ) ) ;
#25122=AXIS2_PLACEMENT_3D ( 'NONE', #64753, #1999, #47095 ) ;
#25139=PLANE ( 'NONE',  #48811 ) ;
#25218=CIRCLE ( 'NONE', #3666, 5.000000000000000888 ) ;
#25310=EDGE_CURVE ( 'NONE', #26473, #46616, #54830, .T. ) ;
#25354=FACE_OUTER_BOUND ( 'NONE', #34458, .T. ) ;
#25479=CARTESIAN_POINT ( 'NONE',  ( 5.000000000000000000, 2.886751345948134428, -2.080000000000000071 ) ) ;
#25632=ORIENTED_EDGE ( 'NONE', *, *, #68449, .F. ) ;
#25640=CARTESIAN_POINT ( 'NONE',  ( -5.000000000000000000, 2.886751345948137981, -5.553418012614792509 ) ) ;
#25664=CARTESIAN_POINT ( 'NONE',  ( -2.260257450329326456, 4.468542444510766209, -0.5197061503823194872 ) ) ;
#25730=CARTESIAN_POINT ( 'NONE',  ( 5.000000000000000888, 0.000000000000000000, -6.000000000000000000 ) ) ;
#25757=UNCERTAINTY_MEASURE_WITH_UNIT (LENGTH_MEASURE( 1.000000000000000082E-05 ), #33274, 'distance_accuracy_value', 'NONE');
#25771=B_SPLINE_CURVE_WITH_KNOTS ( 'NONE', 3,
 ( #28947, #45894, #34966, #6043, #69182, #40607, #40984, #7135, #30048, #5668, #52999, #1536, #24418, #70259 ),
 .UNSPECIFIED., .F., .F.,
 ( 4, 2, 2, 2, 2, 2, 4 ),
 ( 0.01481111731982464805, 0.01564725794959783214, 0.01648339857937101624, 0.01690146889425760829, 0.01731953920914420034, 0.01773760952403079239, 0.01815567983891738443 ),
 .UNSPECIFIED. ) ;
#25942=PRODUCT_DEFINITION_SHAPE ( 'NONE', 'NONE',  #49042 ) ;
#26010=ORIENTED_EDGE ( 'NONE', *, *, #34623, .T. ) ;
#26025=CARTESIAN_POINT ( 'NONE',  ( -4.282125186551308360, 3.301216562737181892, -1.327869168827478408 ) ) ;
#26117=ADVANCED_FACE ( 'NONE', ( #25354 ), #41490, .F. ) ;
#26231=ADVANCED_FACE ( 'NONE', ( #10645 ), #56895, .F. ) ;
#26242=EDGE_LOOP ( 'NONE', ( #36360, #40407 ) ) ;
#26260=AXIS2_PLACEMENT_3D ( 'NONE', #2662, #36087, #59767 ) ;
#26393=DIRECTION ( 'NONE',  ( -0.000000000000000000, -0.000000000000000000, 1.000000000000000000 ) ) ;
#26396=ORIENTED_EDGE ( 'NONE', *, *, #64755, .F. ) ;
#26401=CARTESIAN_POINT ( 'NONE',  ( -1.898848305348268983, 4.677202111653171457, -0.6020238742160447520 ) ) ;
#26473=VERTEX_POINT ( 'NONE', #64381 ) ;
#26538=CARTESIAN_POINT ( 'NONE',  ( -9.974659986866640793E-15, -5.773502691896262640, -5.553418012614792509 ) ) ;
#26720=VERTEX_POINT ( 'NONE', #17642 ) ;
#26945=CARTESIAN_POINT ( 'NONE',  ( -0.8179331680533066251, -5.301268757141566645, -5.826062401966622062 ) ) ;
#26991=CARTESIAN_POINT ( 'NONE',  ( -5.000000000000000000, -4.846777557549235459E-18, -0.5080592402122449114 ) ) ;
#27048=EDGE_CURVE ( 'NONE', #17672, #68345, #51723, .T. ) ;
#27099=CARTESIAN_POINT ( 'NONE',  ( 0.3487148583350060949, -5.572172074566128508, -1.686035282245279765 ) ) ;
#27178=DIRECTION ( 'NONE',  ( 0.000000000000000000, 0.000000000000000000, 1.000000000000000000 ) ) ;
#27394=CIRCLE ( 'NONE', #45464, 3.000000000000000000 ) ;
#27406=EDGE_CURVE ( 'NONE', #3895, #26473, #64529, .T. ) ;
#27426=EDGE_CURVE ( 'NONE', #32014, #18969, #68124, .T. ) ;
#27458=CARTESIAN_POINT ( 'NONE',  ( -5.000000000000000000, -2.886751345948137981, -5.553418012614792509 ) ) ;
#27460=ORIENTED_EDGE ( 'NONE', *, *, #59773, .F. ) ;
#27478=CARTESIAN_POINT ( 'NONE',  ( 3.675296855064185575, -3.651569063273171434, -0.8655517945778166133 ) ) ;
#27608=ADVANCED_FACE ( 'NONE', ( #36457, #69926 ), #47016, .F. ) ;
#27766=EDGE_LOOP ( 'NONE', ( #59642, #38185, #29839, #27460, #56844, #51487, #26010 ) ) ;
#27865=CIRCLE ( 'NONE', #59109, 5.000000000000000888 ) ;
#27923=DIRECTION ( 'NONE',  ( -0.5000000000000006661, 0.8660254037844382635, 0.000000000000000000 ) ) ;
#28078=AXIS2_PLACEMENT_3D ( 'NONE', #28940, #11276, #12015 ) ;
#28470=CARTESIAN_POINT ( 'NONE',  ( 2.925285743277526329, 4.084588180558403891, -5.989444439476610427 ) ) ;
#28520=CARTESIAN_POINT ( 'NONE',  ( 0.7178748134486927501, 5.359037475107204962, -1.327869168827484403 ) ) ;
#28523=ADVANCED_FACE ( 'NONE', ( #67733 ), #4656, .T. ) ;
#28840=CARTESIAN_POINT ( 'NONE',  ( 5.000000000000000000, 1.352381405509861523, -0.8629530094790043293 ) ) ;
#28940=CARTESIAN_POINT ( 'NONE',  ( 0.000000000000000000, 0.000000000000000000, -6.000000000000000000 ) ) ;
#28947=CARTESIAN_POINT ( 'NONE',  ( 5.000000000000000888, -2.886751345948134873, -2.080000000000000071 ) ) ;
#28989=DIRECTION ( 'NONE',  ( 0.000000000000000000, 0.000000000000000000, 1.000000000000000000 ) ) ;
#29033=VECTOR ( 'NONE', #13884, 1000.000000000000000 ) ;
#29145=CARTESIAN_POINT ( 'NONE',  ( 0.000000000000000000, 0.000000000000000000, 0.000000000000000000 ) ) ;
#29206=EDGE_CURVE ( 'NONE', #2617, #40220, #71120, .T. ) ;
#29301=AXIS2_PLACEMENT_3D ( 'NONE', #69084, #10828, #17570 ) ;
#29388=DIRECTION ( 'NONE',  ( 1.000000000000000000, 0.000000000000000000, 0.000000000000000000 ) ) ;
#29459=ORIENTED_EDGE ( 'NONE', *, *, #34623, .F. ) ;
#29559=CARTESIAN_POINT ( 'NONE',  ( 5.000000000000000000, 2.886751345948134428, -2.080000000000000071 ) ) ;
#29658=B_SPLINE_CURVE_WITH_KNOTS ( 'NONE', 3,
 ( #73, #34590, #29676, #52623, #16561, #57172, #22966, #68821, #12031, #17308, #23326, #40241, #57540, #51891 ),
 .UNSPECIFIED., .F., .F.,
 ( 4, 2, 2, 2, 2, 2, 4 ),
 ( 0.01481111731982464805, 0.01564725794959783214, 0.01648339857937101624, 0.01690146889425760829, 0.01731953920914420034, 0.01773760952403079239, 0.01815567983891738443 ),
 .UNSPECIFIED. ) ;
#29676=CARTESIAN_POINT ( 'NONE',  ( -5.000000000000000888, -2.488288133785819589, -1.689848211693934621 ) ) ;
#29712=CARTESIAN_POINT ( 'NONE',  ( -3.351853367131006234, 3.838309248099018411, -6.000000000000003553 ) ) ;
#29789=DIRECTION ( 'NONE',  ( -1.000000000000000000, 0.000000000000000000, 0.000000000000000000 ) ) ;
#29839=ORIENTED_EDGE ( 'NONE', *, *, #32048, .T. ) ;
#29884=CARTESIAN_POINT ( 'NONE',  ( 2.500000000000005773, 4.330127018922191873, -6.000000000000000000 ) ) ;
#29889=CARTESIAN_POINT ( 'NONE',  ( -2.255011273957059359, -4.471571325851515510, -0.5083873451168858804 ) ) ;
#30016=AXIS2_PLACEMENT_3D ( 'NONE', #55399, #73041, #6859 ) ;
#30048=CARTESIAN_POINT ( 'NONE',  ( 5.000000000000000000, -0.9645339558193165574, -0.6919071587033235327 ) ) ;
#30438=DIRECTION ( 'NONE',  ( -0.000000000000000000, -0.000000000000000000, 1.000000000000000000 ) ) ;
#30835=ORIENTED_EDGE ( 'NONE', *, *, #27048, .T. ) ;
#31175=EDGE_LOOP ( 'NONE', ( #44581, #6578, #23406, #3541, #65734 ) ) ;
#31363=ORIENTED_EDGE ( 'NONE', *, *, #9273, .F. ) ;
#31456=ORIENTED_EDGE ( 'NONE', *, *, #32048, .F. ) ;
#31476=DIRECTION ( 'NONE',  ( 1.000000000000000000, 0.000000000000000000, 0.000000000000000000 ) ) ;
#31556=PRESENTATION_STYLE_ASSIGNMENT (( #41377 ) ) ;
#31687=EDGE_LOOP ( 'NONE', ( #35689, #43999, #15895, #39129, #16348 ) ) ;
#31775=AXIS2_PLACEMENT_3D ( 'NONE', #22676, #1269, #56892 ) ;
#31777=DIRECTION ( 'NONE',  ( -0.4415113423096792000, 0.000000000000000000, -0.8972556684757725387 ) ) ;
#31805=ORIENTED_EDGE ( 'NONE', *, *, #68449, .T. ) ;
#31811=DIRECTION ( 'NONE',  ( -0.000000000000000000, -0.000000000000000000, 1.000000000000000000 ) ) ;
#31983=CONICAL_SURFACE ( 'NONE', #74019, 5.000000000000000888, 1.047197551196596299 ) ;
#32014=VERTEX_POINT ( 'NONE', #35206 ) ;
#32048=EDGE_CURVE ( 'NONE', #24152, #40400, #37815, .T. ) ;
#32375=CARTESIAN_POINT ( 'NONE',  ( -1.084202172485504434E-14, -5.773502691896260863, -2.080000000000000071 ) ) ;
#32456=CARTESIAN_POINT ( 'NONE',  ( 5.000000000000000000, 2.886751345948125991, -6.000000000000000000 ) ) ;
#32541=( NAMED_UNIT ( * ) PLANE_ANGLE_UNIT ( ) SI_UNIT ( $, .RADIAN. ) );
#32555=DIRECTION ( 'NONE',  ( 1.000000000000000000, 0.000000000000000000, 0.000000000000000000 ) ) ;
#32598=AXIS2_PLACEMENT_3D ( 'NONE', #21564, #62562, #62176 ) ;
#32802=CARTESIAN_POINT ( 'NONE',  ( -5.000000000000000000, 2.886751345948126879, -2.079999999999992077 ) ) ;
#32890=CONICAL_SURFACE ( 'NONE', #29301, 5.000000000000000888, 1.047197551196596299 ) ;
#33029=ORIENTED_EDGE ( 'NONE', *, *, #10021, .F. ) ;
#33058=CARTESIAN_POINT ( 'NONE',  ( 3.000000000000000000, 0.000000000000000000, -25.03750572909317285 ) ) ;
#33114=CARTESIAN_POINT ( 'NONE',  ( 3.453178355211938388, -3.779809238954861428, -0.7375898304884541679 ) ) ;
#33146=VERTEX_POINT ( 'NONE', #4542 ) ;
#33274=( LENGTH_UNIT ( ) NAMED_UNIT ( * ) SI_UNIT ( .MILLI., .METRE. ) );
#33302=AXIS2_PLACEMENT_3D ( 'NONE', #4275, #27923, #39586 ) ;
#33329=EDGE_CURVE ( 'NONE', #23304, #24152, #13118, .T. ) ;
#33410=AXIS2_PLACEMENT_3D ( 'NONE', #5712, #63225, #28989 ) ;
#33467=CARTESIAN_POINT ( 'NONE',  ( -2.500000000000003997, -4.330127018922192761, -6.000000000000000000 ) ) ;
#33658=AXIS2_PLACEMENT_3D ( 'NONE', #36290, #19369, #18991 ) ;
#33821=VECTOR ( 'NONE', #2308, 1000.000000000000000 ) ;
#33872=CARTESIAN_POINT ( 'NONE',  ( 2.018853055115724882, -4.607917337070903230, -0.5666985376598668855 ) ) ;
#33930=AXIS2_PLACEMENT_3D ( 'NONE', #3213, #2494, #49414 ) ;
#34105=EDGE_CURVE ( 'NONE', #26720, #65774, #25218, .T. ) ;
#34177=CARTESIAN_POINT ( 'NONE',  ( -5.000000000000000000, 2.886751345948137981, -5.553418012614792509 ) ) ;
#34201=VECTOR ( 'NONE', #43636, 1000.000000000000000 ) ;
#34247=AXIS2_PLACEMENT_3D ( 'NONE', #36622, #71190, #8797 ) ;
#34334=DIRECTION ( 'NONE',  ( 0.000000000000000000, 0.000000000000000000, -1.000000000000000000 ) ) ;
#34457=APPLICATION_CONTEXT ( 'automotive_design' ) ;
#34458=EDGE_LOOP ( 'NONE', ( #1152, #63797, #57783, #54990 ) ) ;
#34590=CARTESIAN_POINT ( 'NONE',  ( -4.999999999999999112, -2.691295138309024448, -1.881393335304213821 ) ) ;
#34609=DIRECTION ( 'NONE',  ( 0.000000000000000000, -0.000000000000000000, 1.000000000000000000 ) ) ;
#34623=EDGE_CURVE ( 'NONE', #54553, #47528, #25771, .T. ) ;
#34862=CONICAL_SURFACE ( 'NONE', #54079, 4.749999999999999112, 0.4572823821333981131 ) ;
#34908=B_SPLINE_CURVE_WITH_KNOTS ( 'NONE', 3,
 ( #71140, #65530, #36945, #26025, #59893, #38054, #54251, #20399, #49330, #37699, #25664, #3494, #26401, #9476, #4231, #56474, #5347, #39545, #73364, #22249 ),
 .UNSPECIFIED., .F., .F.,
 ( 4, 2, 2, 2, 2, 2, 2, 2, 2, 4 ),
 ( 2.781148944365360171E-07, 0.0008372784139787578517, 0.001674278713063079033, 0.002511279012147400649, 0.003348279311231721830, 0.003766779460773882204, 0.004185279610316042578, 0.005022279909400362459, 0.005859280208484684074, 0.006696280507569004822 ),
 .UNSPECIFIED. ) ;
#34966=CARTESIAN_POINT ( 'NONE',  ( 5.000000000000000888, -2.488288133785820033, -1.689848211693934621 ) ) ;
#35117=CONICAL_SURFACE ( 'NONE', #2747, 2.449999999999998845, 0.9599310885968813656 ) ;
#35130=EDGE_CURVE ( 'NONE', #18028, #36077, #24016, .T. ) ;
#35165=( GEOMETRIC_REPRESENTATION_CONTEXT ( 3 ) GLOBAL_UNCERTAINTY_ASSIGNED_CONTEXT ( ( #14474 ) ) GLOBAL_UNIT_ASSIGNED_CONTEXT ( ( #49830, #10356, #74249 ) ) REPRESENTATION_CONTEXT ( 'NONE', 'WORKASPACE' ) );
#35166=ORIENTED_EDGE ( 'NONE', *, *, #14309, .T. ) ;
#35175=CARTESIAN_POINT ( 'NONE',  ( -1.324703144935793775, -5.008684974571242066, -0.8655517945778401501 ) ) ;
#35182=CIRCLE ( 'NONE', #5200, 2.500000000000000000 ) ;
#35206=CARTESIAN_POINT ( 'NONE',  ( 2.500000000000003109, -4.330127018922192761, -6.000000000000000000 ) ) ;
#35537=CARTESIAN_POINT ( 'NONE',  ( -0.3476802294499993229, -5.572769417831399785, -1.687189089856318880 ) ) ;
#35619=CARTESIAN_POINT ( 'NONE',  ( 5.000000000000000000, 2.886751345948137981, -5.553418012614792509 ) ) ;
#35689=ORIENTED_EDGE ( 'NONE', *, *, #39044, .T. ) ;
#35905=CARTESIAN_POINT ( 'NONE',  ( -1.084202172485504434E-14, -5.773502691896260863, -2.080000000000000071 ) ) ;
#35940=EDGE_LOOP ( 'NONE', ( #3979, #72535, #25632, #47690, #15453 ) ) ;
#35973=ORIENTED_EDGE ( 'NONE', *, *, #23005, .F. ) ;
#36073=CARTESIAN_POINT ( 'NONE',  ( 0.000000000000000000, 0.000000000000000000, -6.000000000000000000 ) ) ;
#36077=VERTEX_POINT ( 'NONE', #61838 ) ;
#36087=DIRECTION ( 'NONE',  ( -0.000000000000000000, -0.000000000000000000, 1.000000000000000000 ) ) ;
#36152=DIRECTION ( 'NONE',  ( 1.000000000000000000, 0.000000000000000000, 0.000000000000000000 ) ) ;
#36154=CARTESIAN_POINT ( 'NONE',  ( 0.000000000000000000, 0.000000000000000000, -6.000000000000000000 ) ) ;
#36187=EDGE_CURVE ( 'NONE', #23304, #47528, #23829, .T. ) ;
#36290=CARTESIAN_POINT ( 'NONE',  ( 0.000000000000000000, 0.000000000000000000, -6.000000000000000000 ) ) ;
#36360=ORIENTED_EDGE ( 'NONE', *, *, #64755, .T. ) ;
#36413=EDGE_LOOP ( 'NONE', ( #56106, #59097, #13478 ) ) ;
#36457=FACE_BOUND ( 'NONE', #55181, .T. ) ;
#36601=VERTEX_POINT ( 'NONE', #1590 ) ;
#36622=CARTESIAN_POINT ( 'NONE',  ( 0.000000000000000000, 0.000000000000000000, -5.974599999999999689 ) ) ;
#36807=FACE_OUTER_BOUND ( 'NONE', #66298, .T. ) ;
#36823=LINE ( 'NONE', #1556, #29033 ) ;
#36831=FILL_AREA_STYLE ('',( #8644 ) ) ;
#36945=CARTESIAN_POINT ( 'NONE',  ( -4.652319770550016109, 3.087484620012986625, -1.687189089856314217 ) ) ;
#37062=AXIS2_PLACEMENT_3D ( 'NONE', #66364, #43062, #71603 ) ;
#37217=CARTESIAN_POINT ( 'NONE',  ( 0.000000000000000000, 0.000000000000000000, -6.000000000000000000 ) ) ;
#37260=ORIENTED_EDGE ( 'NONE', *, *, #70512, .F. ) ;
#37452=VECTOR ( 'NONE', #12171, 999.9999999999998863 ) ;
#37511=CYLINDRICAL_SURFACE ( 'NONE', #62875, 2.500000000000000000 ) ;
#37699=CARTESIAN_POINT ( 'NONE',  ( -2.381231458764688558, 4.398698068175660225, -0.5078976954042897507 ) ) ;
#37727=ORIENTED_EDGE ( 'NONE', *, *, #41679, .T. ) ;
#37758=ORIENTED_EDGE ( 'NONE', *, *, #24271, .T. ) ;
#37815=LINE ( 'NONE', #72374, #52758 ) ;
#37936=ORIENTED_EDGE ( 'NONE', *, *, #56017, .F. ) ;
#38010=CARTESIAN_POINT ( 'NONE',  ( -2.925285743277526329, -4.084588180558410109, -5.989444439476605986 ) ) ;
#38054=CARTESIAN_POINT ( 'NONE',  ( -3.675296855064184687, 3.651569063273166993, -0.8655517945778067324 ) ) ;
#38067=AXIS2_PLACEMENT_3D ( 'NONE', #12050, #40633, #23346 ) ;
#38185=ORIENTED_EDGE ( 'NONE', *, *, #802, .F. ) ;
#38300=ADVANCED_FACE ( 'NONE', ( #9694 ), #25139, .T. ) ;
#38376=ORIENTED_EDGE ( 'NONE', *, *, #3249, .T. ) ;
#38512=VERTEX_POINT ( 'NONE', #67208 ) ;
#38632=CARTESIAN_POINT ( 'NONE',  ( 3.035766082959412415E-15, 5.773502691896260863, -2.080000000000000071 ) ) ;
#38739=ORIENTED_EDGE ( 'NONE', *, *, #59773, .T. ) ;
#38753=MECHANICAL_DESIGN_GEOMETRIC_PRESENTATION_REPRESENTATION('',(#23159),#35165);
#38825=ORIENTED_EDGE ( 'NONE', *, *, #52822, .T. ) ;
#39044=EDGE_CURVE ( 'NONE', #68345, #13774, #59728, .T. ) ;
#39129=ORIENTED_EDGE ( 'NONE', *, *, #41254, .F. ) ;
#39296=ORIENTED_EDGE ( 'NONE', *, *, #10942, .T. ) ;
#39445=CIRCLE ( 'NONE', #58639, 3.000000000000000000 ) ;
#39523=CARTESIAN_POINT ( 'NONE',  ( 2.260257450329328233, -4.468542444510769762, -0.5197061503823295903 ) ) ;
#39545=CARTESIAN_POINT ( 'NONE',  ( -0.3487148583350038744, 5.572172074566123179, -1.686035282245269995 ) ) ;
#39586=DIRECTION ( 'NONE',  ( -0.8660254037844382635, -0.5000000000000006661, 0.000000000000000000 ) ) ;
#39670=ADVANCED_FACE ( 'NONE', ( #22003 ), #48967, .F. ) ;
#39690=SURFACE_STYLE_FILL_AREA ( #67879 ) ;
#39777=CARTESIAN_POINT ( 'NONE',  ( 4.180704885107411783, 3.359771601077109260, -5.801655677627843843 ) ) ;
#39843=LINE ( 'NONE', #33058, #9514 ) ;
#39865=VERTEX_POINT ( 'NONE', #42179 ) ;
#39866=UNCERTAINTY_MEASURE_WITH_UNIT (LENGTH_MEASURE( 1.000000000000000082E-05 ), #7166, 'distance_accuracy_value', 'NONE');
#39901=EDGE_CURVE ( 'NONE', #36077, #46616, #27394, .T. ) ;
#40081=CARTESIAN_POINT ( 'NONE',  ( -4.279208249584786294, -3.302900657080020341, -1.325189086772939895 ) ) ;
#40138=CARTESIAN_POINT ( 'NONE',  ( 3.556264818047235821, 3.720292241887089624, -5.918341802876230240 ) ) ;
#40163=VECTOR ( 'NONE', #3355, 999.9999999999998863 ) ;
#40192=CARTESIAN_POINT ( 'NONE',  ( 2.739742549670660665, 4.191711593333631747, -0.5197061503823161566 ) ) ;
#40213=DIRECTION ( 'NONE',  ( 0.000000000000000000, 0.000000000000000000, 1.000000000000000000 ) ) ;
#40220=VERTEX_POINT ( 'NONE', #51882 ) ;
#40241=CARTESIAN_POINT ( 'NONE',  ( -5.000000000000000000, -0.2835658343809315807, -0.5205273423269579647 ) ) ;
#40400=VERTEX_POINT ( 'NONE', #26991 ) ;
#40407=ORIENTED_EDGE ( 'NONE', *, *, #9569, .T. ) ;
#40552=CARTESIAN_POINT ( 'NONE',  ( 3.667169054266697703, 3.656261651251516032, -0.8603634151101352545 ) ) ;
#40607=CARTESIAN_POINT ( 'NONE',  ( 5.000000000000000000, -1.472375319565264684, -0.9369361380397587258 ) ) ;
#40630=ORIENTED_EDGE ( 'NONE', *, *, #27426, .F. ) ;
#40633=DIRECTION ( 'NONE',  ( -0.000000000000000000, -0.000000000000000000, 1.000000000000000000 ) ) ;
#40661=ORIENTED_EDGE ( 'NONE', *, *, #47490, .T. ) ;
#40666=CIRCLE ( 'NONE', #37062, 3.000000000000000000 ) ;
#40874=CARTESIAN_POINT ( 'NONE',  ( 5.000000000000000000, 1.101175676120959901, -0.7375066809288793879 ) ) ;
#40940=CARTESIAN_POINT ( 'NONE',  ( -3.000000000000000000, 3.673940397442059868E-16, -25.03750572909317285 ) ) ;
#40984=CARTESIAN_POINT ( 'NONE',  ( 5.000000000000000000, -1.349638343847295419, -0.8687551798607463516 ) ) ;
#41017=CARTESIAN_POINT ( 'NONE',  ( -3.000000000000000000, 3.673940397442059868E-16, 0.000000000000000000 ) ) ;
#41198=EDGE_CURVE ( 'NONE', #33146, #26720, #63662, .T. ) ;
#41254=EDGE_CURVE ( 'NONE', #65774, #33146, #10630, .T. ) ;
#41377=SURFACE_STYLE_USAGE ( .BOTH. , #24096 ) ;
#41490=CONICAL_SURFACE ( 'NONE', #34247, 3.000000000000000000, 0.9599310885968762586 ) ;
#41496=ORIENTED_EDGE ( 'NONE', *, *, #60838, .F. ) ;
#41558=FACE_OUTER_BOUND ( 'NONE', #6032, .T. ) ;
#41652=CARTESIAN_POINT ( 'NONE',  ( 4.279208249584789847, 3.302900657080011459, -1.325189086772932123 ) ) ;
#41679=EDGE_CURVE ( 'NONE', #24699, #54553, #64771, .T. ) ;
#41832=EDGE_CURVE ( 'NONE', #45184, #38512, #20742, .T. ) ;
#42013=CARTESIAN_POINT ( 'NONE',  ( 1.653121499799246719, -4.819072548984012272, -5.948595712916168843 ) ) ;
#42179=CARTESIAN_POINT ( 'NONE',  ( -2.500000000000003997, -4.330127018922192761, -6.000000000000000000 ) ) ;
#42304=EDGE_LOOP ( 'NONE', ( #67322, #2638, #61478, #42930 ) ) ;
#42316=DIRECTION ( 'NONE',  ( 0.5000000000000006661, -0.8660254037844383745, 0.000000000000000000 ) ) ;
#42357=ORIENTED_EDGE ( 'NONE', *, *, #70512, .T. ) ;
#42418=LINE ( 'NONE', #13824, #49866 ) ;
#42430=ADVANCED_FACE ( 'NONE', ( #41558 ), #8089, .T. ) ;
#42441=DIRECTION ( 'NONE',  ( -0.000000000000000000, -0.000000000000000000, 1.000000000000000000 ) ) ;
#42595=AXIS2_PLACEMENT_3D ( 'NONE', #51176, #57941, #46289 ) ;
#42805=DIRECTION ( 'NONE',  ( 0.000000000000000000, 0.000000000000000000, 1.000000000000000000 ) ) ;
#42882=CARTESIAN_POINT ( 'NONE',  ( 5.000000000000002665, -2.886751345948134873, -5.553418012614792509 ) ) ;
#42930=ORIENTED_EDGE ( 'NONE', *, *, #485, .F. ) ;
#42942=LINE ( 'NONE', #59125, #9129 ) ;
#43043=ORIENTED_EDGE ( 'NONE', *, *, #838, .T. ) ;
#43062=DIRECTION ( 'NONE',  ( 0.000000000000000000, -0.000000000000000000, 1.000000000000000000 ) ) ;
#43132=CARTESIAN_POINT ( 'NONE',  ( 2.074714256722481664, -4.575665857285986959, -5.989444439476606874 ) ) ;
#43159=CARTESIAN_POINT ( 'NONE',  ( -9.974659986866640793E-15, -5.773502691896262640, -5.553418012614792509 ) ) ;
#43191=CARTESIAN_POINT ( 'NONE',  ( -5.000000000000000000, 2.886751345948126879, -6.000000000000000000 ) ) ;
#43262=VECTOR ( 'NONE', #48934, 1000.000000000000000 ) ;
#43279=ADVANCED_FACE ( 'NONE', ( #51922 ), #10582, .T. ) ;
#43395=AXIS2_PLACEMENT_3D ( 'NONE', #48320, #71232, #19735 ) ;
#43501=B_SPLINE_CURVE_WITH_KNOTS ( 'NONE', 3,
 ( #43159, #26945, #3312, #60808 ),
 .UNSPECIFIED., .F., .F.,
 ( 4, 4 ),
 ( 2.380735200943099693E-07, 0.002921158011986722466 ),
 .UNSPECIFIED. ) ;
#43636=DIRECTION ( 'NONE',  ( 0.000000000000000000, 0.000000000000000000, 1.000000000000000000 ) ) ;
#43929=ORIENTED_EDGE ( 'NONE', *, *, #49891, .T. ) ;
#43999=ORIENTED_EDGE ( 'NONE', *, *, #69699, .T. ) ;
#44029=CARTESIAN_POINT ( 'NONE',  ( -4.592054218142291866, -3.122278952918454031, -5.689399939901067071 ) ) ;
#44214=DIRECTION ( 'NONE',  ( 0.000000000000000000, 0.000000000000000000, 1.000000000000000000 ) ) ;
#44403=CARTESIAN_POINT ( 'NONE',  ( -3.556264818047238485, -3.720292241887096285, -5.918341802876226687 ) ) ;
#44421=CARTESIAN_POINT ( 'NONE',  ( 5.000000000000000888, -2.886751345948134873, -2.080000000000000071 ) ) ;
#44466=CARTESIAN_POINT ( 'NONE',  ( -5.000000000000000000, -2.886751345948137981, -5.553418012614792509 ) ) ;
#44574=APPLICATION_CONTEXT ( 'automotive_design' ) ;
#44575=CARTESIAN_POINT ( 'NONE',  ( 5.000000000000000000, 2.886751345948125991, -6.000000000000000000 ) ) ;
#44581=ORIENTED_EDGE ( 'NONE', *, *, #22646, .T. ) ;
#44728=CARTESIAN_POINT ( 'NONE',  ( 0.000000000000000000, 0.000000000000000000, 0.000000000000000000 ) ) ;
#44777=CARTESIAN_POINT ( 'NONE',  ( -2.712167343862821323, -4.207632145829752979, -6.000000000000000888 ) ) ;
#45039=ORIENTED_EDGE ( 'NONE', *, *, #56301, .T. ) ;
#45051=CARTESIAN_POINT ( 'NONE',  ( 5.000000000000000888, -2.886751345948134873, -2.080000000000000071 ) ) ;
#45096=CARTESIAN_POINT ( 'NONE',  ( 0.1709976663248966577, 5.674777143212787145, -1.879366290983712107 ) ) ;
#45163=CARTESIAN_POINT ( 'NONE',  ( 4.282125186551308360, -3.301216562737187221, -1.327869168827487290 ) ) ;
#45184=VERTEX_POINT ( 'NONE', #44466 ) ;
#45274=FACE_OUTER_BOUND ( 'NONE', #73765, .T. ) ;
#45464=AXIS2_PLACEMENT_3D ( 'NONE', #24503, #47440, #36152 ) ;
#45474=CARTESIAN_POINT ( 'NONE',  ( 1.324703144935786447, 5.008684974571240289, -0.8655517945778323785 ) ) ;
#45478=DIRECTION ( 'NONE',  ( 0.000000000000000000, 0.000000000000000000, -1.000000000000000000 ) ) ;
#45512=FACE_OUTER_BOUND ( 'NONE', #55553, .T. ) ;
#45638=ORIENTED_EDGE ( 'NONE', *, *, #36187, .T. ) ;
#45781=VECTOR ( 'NONE', #12347, 1000.000000000000000 ) ;
#45819=CARTESIAN_POINT ( 'NONE',  ( -4.999999999999999112, -2.417244626924490269, -5.688952927922134251 ) ) ;
#45837=CONICAL_SURFACE ( 'NONE', #46996, 4.749999999999999112, 0.4572823821333981131 ) ;
#45894=CARTESIAN_POINT ( 'NONE',  ( 4.999999999999999112, -2.691295138309024892, -1.881393335304215153 ) ) ;
#45965=VERTEX_POINT ( 'NONE', #26538 ) ;
#46088=CARTESIAN_POINT ( 'NONE',  ( 5.000000000000000000, 6.074766241781102566E-16, -0.5080592402122449114 ) ) ;
#46091=EDGE_LOOP ( 'NONE', ( #29459, #65935, #73586, #39296, #31805, #68285 ) ) ;
#46202=CARTESIAN_POINT ( 'NONE',  ( -5.000000000000000000, 2.886751345948126879, -2.079999999999992077 ) ) ;
#46289=DIRECTION ( 'NONE',  ( 1.000000000000000000, 0.000000000000000000, 0.000000000000000000 ) ) ;
#46367=ORIENTED_EDGE ( 'NONE', *, *, #56017, .T. ) ;
#46382=CLOSED_SHELL ( 'NONE', ( #47762, #26117, #21765, #1012, #18764, #6458, #54087, #15892, #26231, #42430, #38300, #43279, #27608, #61796, #21717, #14580, #16915, #16372, #28523, #61217, #47940, #39670, #46551, #59241 ) ) ;
#46396=AXIS2_PLACEMENT_3D ( 'NONE', #32456, #21169, #27178 ) ;
#46544=CARTESIAN_POINT ( 'NONE',  ( 4.999999999999999112, 0.4881033300985041512, -6.000000000000000000 ) ) ;
#46551=ADVANCED_FACE ( 'NONE', ( #3920 ), #36, .F. ) ;
#46616=VERTEX_POINT ( 'NONE', #6140 ) ;
#46833=CARTESIAN_POINT ( 'NONE',  ( 0.8179331680532997417, 5.301268757141563981, -5.826062401966623838 ) ) ;
#46838=CARTESIAN_POINT ( 'NONE',  ( -0.7178748134487012988, -5.359037475107207626, -1.327869168827489732 ) ) ;
#46996=AXIS2_PLACEMENT_3D ( 'NONE', #182, #34334, #29789 ) ;
#47016=PLANE ( 'NONE',  #17680 ) ;
#47095=DIRECTION ( 'NONE',  ( -1.000000000000000000, 0.000000000000000000, 0.000000000000000000 ) ) ;
#47140=( GEOMETRIC_REPRESENTATION_CONTEXT ( 3 ) GLOBAL_UNCERTAINTY_ASSIGNED_CONTEXT ( ( #25757 ) ) GLOBAL_UNIT_ASSIGNED_CONTEXT ( ( #33274, #32541, #50954 ) ) REPRESENTATION_CONTEXT ( 'NONE', 'WORKASPACE' ) );
#47291=ORIENTED_EDGE ( 'NONE', *, *, #802, .T. ) ;
#47334=EDGE_LOOP ( 'NONE', ( #37260, #71928, #5839, #6817 ) ) ;
#47440=DIRECTION ( 'NONE',  ( -0.000000000000000000, -0.000000000000000000, 1.000000000000000000 ) ) ;
#47490=EDGE_CURVE ( 'NONE', #26473, #3895, #13340, .T. ) ;
#47528=VERTEX_POINT ( 'NONE', #46088 ) ;
#47665=CARTESIAN_POINT ( 'NONE',  ( 0.000000000000000000, 0.000000000000000000, -6.000000000000000000 ) ) ;
#47690=ORIENTED_EDGE ( 'NONE', *, *, #16842, .F. ) ;
#47718=VERTEX_POINT ( 'NONE', #49763 ) ;
#47745=( NAMED_UNIT ( * ) SI_UNIT ( $, .STERADIAN. ) SOLID_ANGLE_UNIT ( ) );
#47762=ADVANCED_FACE ( 'NONE', ( #55789 ), #22319, .F. ) ;
#47940=ADVANCED_FACE ( 'NONE', ( #51629 ), #45837, .T. ) ;
#48025=CARTESIAN_POINT ( 'NONE',  ( 5.000000000000000000, 1.947085426416884202, -5.800379292880308846 ) ) ;
#48156=ORIENTED_EDGE ( 'NONE', *, *, #3249, .F. ) ;
#48213=CARTESIAN_POINT ( 'NONE',  ( -5.000000000000000000, -2.886751345948133540, -6.000000000000000000 ) ) ;
#48319=PRODUCT_DEFINITION_CONTEXT ( 'detailed design', #44574, 'design' ) ;
#48320=CARTESIAN_POINT ( 'NONE',  ( 0.000000000000000000, 0.000000000000000000, 0.000000000000000000 ) ) ;
#48380=CARTESIAN_POINT ( 'NONE',  ( 1.443735181952766844, -4.939961795957303003, -5.918341802876224911 ) ) ;
#48432=ORIENTED_EDGE ( 'NONE', *, *, #41832, .T. ) ;
#48811=AXIS2_PLACEMENT_3D ( 'NONE', #70980, #65367, #20606 ) ;
#48934=DIRECTION ( 'NONE',  ( 0.000000000000000000, 0.000000000000000000, 1.000000000000000000 ) ) ;
#48967=CONICAL_SURFACE ( 'NONE', #68205, 2.449999999999998845, 0.9599310885968813656 ) ;
#49042=PRODUCT_DEFINITION ( 'UNKNOWN', '', #15990, #48319 ) ;
#49100=LINE ( 'NONE', #21254, #64433 ) ;
#49262=B_SPLINE_CURVE_WITH_KNOTS ( 'NONE', 3,
 ( #49967, #71784, #72888, #14650 ),
 .UNSPECIFIED., .F., .F.,
 ( 4, 4 ),
 ( 2.380735200807732181E-07, 0.002921158011986708155 ),
 .UNSPECIFIED. ) ;
#49318=EDGE_CURVE ( 'NONE', #18969, #26720, #69943, .T. ) ;
#49330=CARTESIAN_POINT ( 'NONE',  ( -2.744988726042923766, 4.188682711992889551, -0.5083873451168725577 ) ) ;
#49414=DIRECTION ( 'NONE',  ( 1.000000000000000000, 0.000000000000000000, 0.000000000000000000 ) ) ;
#49598=DIRECTION ( 'NONE',  ( -0.000000000000000000, -0.000000000000000000, 1.000000000000000000 ) ) ;
#49763=CARTESIAN_POINT ( 'NONE',  ( -1.084202172485504434E-14, -5.773502691896260863, -2.080000000000000071 ) ) ;
#49774=CARTESIAN_POINT ( 'NONE',  ( 0.000000000000000000, 0.000000000000000000, -6.000000000000000000 ) ) ;
#49830=( LENGTH_UNIT ( ) NAMED_UNIT ( * ) SI_UNIT ( .MILLI., .METRE. ) );
#49866=VECTOR ( 'NONE', #2967, 999.9999999999998863 ) ;
#49891=EDGE_CURVE ( 'NONE', #70907, #55045, #35182, .T. ) ;
#49967=CARTESIAN_POINT ( 'NONE',  ( 5.000000000000002665, -2.886751345948134873, -5.553418012614792509 ) ) ;
#50002=ORIENTED_EDGE ( 'NONE', *, *, #838, .F. ) ;
#50031=CARTESIAN_POINT ( 'NONE',  ( 0.1714266706912579152, -5.674529457426388923, -1.878862934774795823 ) ) ;
#50048=CARTESIAN_POINT ( 'NONE',  ( 0.000000000000000000, 0.000000000000000000, -6.000000000000000000 ) ) ;
#50526=B_SPLINE_CURVE_WITH_KNOTS ( 'NONE', 3,
 ( #69945, #22620, #29712, #62489 ),
 .UNSPECIFIED., .F., .F.,
 ( 4, 4 ),
 ( 2.380735200870747991E-07, 0.002921158011986710323 ),
 .UNSPECIFIED. ) ;
#50664=CARTESIAN_POINT ( 'NONE',  ( 2.500000000000005773, 4.330127018922191873, -6.000000000000000000 ) ) ;
#50893=DIRECTION ( 'NONE',  ( 1.000000000000000000, 0.000000000000000000, 0.000000000000000000 ) ) ;
#50954=( NAMED_UNIT ( * ) SI_UNIT ( $, .STERADIAN. ) SOLID_ANGLE_UNIT ( ) );
#50965=VECTOR ( 'NONE', #40213, 1000.000000000000000 ) ;
#51093=CARTESIAN_POINT ( 'NONE',  ( 0.000000000000000000, 0.000000000000000000, -6.000000000000000000 ) ) ;
#51176=CARTESIAN_POINT ( 'NONE',  ( 0.000000000000000000, 0.000000000000000000, -0.3501037691048548561 ) ) ;
#51224=PLANE ( 'NONE',  #33302 ) ;
#51316=AXIS2_PLACEMENT_3D ( 'NONE', #63208, #34609, #23704 ) ;
#51405=CARTESIAN_POINT ( 'NONE',  ( 5.000000000000000000, 2.886751345948137981, -5.553418012614792509 ) ) ;
#51455=CARTESIAN_POINT ( 'NONE',  ( -5.000000000000000000, 1.101175676120956348, -0.7375066809288767233 ) ) ;
#51459=CARTESIAN_POINT ( 'NONE',  ( 2.008727693139922721, 4.613763217533267458, -0.5592653008974296514 ) ) ;
#51460=DIRECTION ( 'NONE',  ( -1.000000000000000000, 0.000000000000000000, 0.000000000000000000 ) ) ;
#51487=ORIENTED_EDGE ( 'NONE', *, *, #4273, .F. ) ;
#51629=FACE_OUTER_BOUND ( 'NONE', #27766, .T. ) ;
#51723=B_SPLINE_CURVE_WITH_KNOTS ( 'NONE', 3,
 ( #11398, #23069, #68925, #52736, #1286, #25640 ),
 .UNSPECIFIED., .F., .F.,
 ( 4, 2, 4 ),
 ( 0.008070708573309213693, 0.009531758523483287518, 0.01099280847365736134 ),
 .UNSPECIFIED. ) ;
#51776=CARTESIAN_POINT ( 'NONE',  ( 5.000000000000000000, 2.059541880722000506, -1.329159518034687126 ) ) ;
#51863=B_SPLINE_CURVE_WITH_KNOTS ( 'NONE', 3,
 ( #64572, #46544, #1829, #48025, #13059, #35619 ),
 .UNSPECIFIED., .F., .F.,
 ( 4, 2, 4 ),
 ( 0.008070708573309213693, 0.009531758523483289253, 0.01099280847365736308 ),
 .UNSPECIFIED. ) ;
#51882=CARTESIAN_POINT ( 'NONE',  ( 5.000000000000000000, 2.886751345948134428, -2.080000000000000071 ) ) ;
#51891=CARTESIAN_POINT ( 'NONE',  ( -5.000000000000000000, -4.846777557549235459E-18, -0.5080592402122449114 ) ) ;
#51913=CONICAL_SURFACE ( 'NONE', #33930, 5.000000000000000888, 1.047197551196596299 ) ;
#51922=FACE_OUTER_BOUND ( 'NONE', #10284, .T. ) ;
#52092=CARTESIAN_POINT ( 'NONE',  ( -2.618768541235303005, -4.261555969668739507, -0.5078976954042990766 ) ) ;
#52331=DIRECTION ( 'NONE',  ( 0.000000000000000000, -0.000000000000000000, 1.000000000000000000 ) ) ;
#52447=CARTESIAN_POINT ( 'NONE',  ( -0.4079457818577069683, 5.537975084925943037, -5.689399939901069736 ) ) ;
#52455=CARTESIAN_POINT ( 'NONE',  ( -4.084562121000262280, -3.415279651815011253, -1.156968425231159614 ) ) ;
#52623=CARTESIAN_POINT ( 'NONE',  ( -4.999999999999998224, -2.058885705017527989, -1.328630925609301183 ) ) ;
#52690=ORIENTED_EDGE ( 'NONE', *, *, #27048, .F. ) ;
#52736=CARTESIAN_POINT ( 'NONE',  ( -5.000000000000000000, 1.947085426416883980, -5.800379292880308846 ) ) ;
#52758=VECTOR ( 'NONE', #31777, 999.9999999999998863 ) ;
#52822=EDGE_CURVE ( 'NONE', #3895, #55045, #22172, .T. ) ;
#52943=DIRECTION ( 'NONE',  ( 1.000000000000000000, 0.000000000000000000, 0.000000000000000000 ) ) ;
#52949=( GEOMETRIC_REPRESENTATION_CONTEXT ( 3 ) GLOBAL_UNCERTAINTY_ASSIGNED_CONTEXT ( ( #39866 ) ) GLOBAL_UNIT_ASSIGNED_CONTEXT ( ( #7166, #59044, #47745 ) ) REPRESENTATION_CONTEXT ( 'NONE', 'WORKASPACE' ) );
#52999=CARTESIAN_POINT ( 'NONE',  ( 5.000000000000000000, -0.5603747650654238299, -0.5678343202077608121 ) ) ;
#53201=CARTESIAN_POINT ( 'NONE',  ( -1.653121499799246497, 4.819072548984005167, -5.948595712916174172 ) ) ;
#53204=EDGE_CURVE ( 'NONE', #47718, #38512, #64922, .T. ) ;
#53396=DIRECTION ( 'NONE',  ( -0.000000000000000000, -0.000000000000000000, 1.000000000000000000 ) ) ;
#53401=LINE ( 'NONE', #3041, #33821 ) ;
#53733=DIRECTION ( 'NONE',  ( -0.000000000000000000, -0.000000000000000000, 1.000000000000000000 ) ) ;
#54079=AXIS2_PLACEMENT_3D ( 'NONE', #44728, #45478, #63143 ) ;
#54087=ADVANCED_FACE ( 'NONE', ( #21915 ), #51224, .T. ) ;
#54251=CARTESIAN_POINT ( 'NONE',  ( -3.453178355211937944, 3.779809238954856099, -0.7375898304884446199 ) ) ;
#54553=VERTEX_POINT ( 'NONE', #45051 ) ;
#54779=PLANE ( 'NONE',  #21299 ) ;
#54795=B_SPLINE_CURVE_WITH_KNOTS ( 'NONE', 3,
 ( #58517, #7012, #17557, #40874, #28840, #18657, #51776, #24316, #320, #29559 ),
 .UNSPECIFIED., .F., .F.,
 ( 4, 2, 2, 2, 4 ),
 ( 0.01815567983891738443, 0.01899359644517026671, 0.01983151305142315246, 0.02066942965767603474, 0.02150734626392891702 ),
 .UNSPECIFIED. ) ;
#54830=LINE ( 'NONE', #55573, #40163 ) ;
#54990=ORIENTED_EDGE ( 'NONE', *, *, #58136, .F. ) ;
#55045=VERTEX_POINT ( 'NONE', #10366 ) ;
#55181=EDGE_LOOP ( 'NONE', ( #33029, #55836 ) ) ;
#55299=STYLED_ITEM ( 'NONE', ( #31556 ), #11785 ) ;
#55381=PRODUCT ( 'torque nut 03_iso_ISO 7042-M6-N', 'torque nut 03_iso_ISO 7042-M6-N', '', ( #67038 ) ) ;
#55397=CARTESIAN_POINT ( 'NONE',  ( -5.000000000000000000, 0.000000000000000000, -6.000000000000000000 ) ) ;
#55399=CARTESIAN_POINT ( 'NONE',  ( 0.000000000000000000, 0.000000000000000000, -5.974599999999999689 ) ) ;
#55484=SURFACE_SIDE_STYLE ('',( #39690 ) ) ;
#55512=ORIENTED_EDGE ( 'NONE', *, *, #33329, .F. ) ;
#55519=AXIS2_PLACEMENT_3D ( 'NONE', #29145, #62655, #73899 ) ;
#55553=EDGE_LOOP ( 'NONE', ( #43043, #24484, #14535 ) ) ;
#55573=CARTESIAN_POINT ( 'NONE',  ( 3.000000000000000000, 3.673940397442059868E-16, -5.974599999999999689 ) ) ;
#55663=VERTEX_POINT ( 'NONE', #41017 ) ;
#55691=CARTESIAN_POINT ( 'NONE',  ( 1.898848305348270982, -4.677202111653177674, -0.6020238742160556322 ) ) ;
#55789=FACE_OUTER_BOUND ( 'NONE', #72802, .T. ) ;
#55800=DIRECTION ( 'NONE',  ( -0.000000000000000000, -0.000000000000000000, 1.000000000000000000 ) ) ;
#55836=ORIENTED_EDGE ( 'NONE', *, *, #15121, .F. ) ;
#55844=DIRECTION ( 'NONE',  ( -0.8660254037844380415, 0.5000000000000008882, 0.000000000000000000 ) ) ;
#55891=FACE_OUTER_BOUND ( 'NONE', #23589, .T. ) ;
#56017=EDGE_CURVE ( 'NONE', #40400, #13774, #23767, .T. ) ;
#56062=CARTESIAN_POINT ( 'NONE',  ( 2.991272306860053298, -4.046490820311139380, -0.5592653008974324269 ) ) ;
#56106=ORIENTED_EDGE ( 'NONE', *, *, #16842, .T. ) ;
#56301=EDGE_CURVE ( 'NONE', #45965, #39865, #43501, .T. ) ;
#56474=CARTESIAN_POINT ( 'NONE',  ( -0.9154378789997292820, 5.244974386029388036, -1.156968425231163167 ) ) ;
#56600=PLANE ( 'NONE',  #62841 ) ;
#56766=DIRECTION ( 'NONE',  ( -0.000000000000000000, -0.000000000000000000, 1.000000000000000000 ) ) ;
#56844=ORIENTED_EDGE ( 'NONE', *, *, #53204, .F. ) ;
#56892=DIRECTION ( 'NONE',  ( 1.000000000000000000, 0.000000000000000000, 0.000000000000000000 ) ) ;
#56895=PLANE ( 'NONE',  #46396 ) ;
#56947=EDGE_CURVE ( 'NONE', #68345, #65774, #50526, .T. ) ;
#57172=CARTESIAN_POINT ( 'NONE',  ( -5.000000000000000000, -1.472375319565265794, -0.9369361380397573935 ) ) ;
#57480=CARTESIAN_POINT ( 'NONE',  ( -4.999999999999999112, 2.059541880721995177, -1.329159518034682685 ) ) ;
#57540=CARTESIAN_POINT ( 'NONE',  ( -5.000000000000000000, -0.1416384297035285789, -0.5080592402122394713 ) ) ;
#57783=ORIENTED_EDGE ( 'NONE', *, *, #39901, .F. ) ;
#57805=CARTESIAN_POINT ( 'NONE',  ( 2.712167343862820434, 4.207632145829745873, -6.000000000000002665 ) ) ;
#57941=DIRECTION ( 'NONE',  ( 0.000000000000000000, 0.000000000000000000, -1.000000000000000000 ) ) ;
#58105=DIRECTION ( 'NONE',  ( -0.000000000000000000, -0.000000000000000000, 1.000000000000000000 ) ) ;
#58136=EDGE_CURVE ( 'NONE', #3895, #36077, #42418, .T. ) ;
#58473=CARTESIAN_POINT ( 'NONE',  ( -3.101151694651716806, -3.983051926191232717, -0.6020238742160465284 ) ) ;
#58517=CARTESIAN_POINT ( 'NONE',  ( 5.000000000000000000, 6.074766241781102566E-16, -0.5080592402122449114 ) ) ;
#58639=AXIS2_PLACEMENT_3D ( 'NONE', #60052, #31811, #32555 ) ;
#58685=CARTESIAN_POINT ( 'NONE',  ( 5.000000000000000000, -0.4878135028931873673, -6.000000000000001776 ) ) ;
#59041=DIRECTION ( 'NONE',  ( 0.000000000000000000, 0.000000000000000000, -1.000000000000000000 ) ) ;
#59044=( NAMED_UNIT ( * ) PLANE_ANGLE_UNIT ( ) SI_UNIT ( $, .RADIAN. ) );
#59097=ORIENTED_EDGE ( 'NONE', *, *, #10942, .F. ) ;
#59109=AXIS2_PLACEMENT_3D ( 'NONE', #51093, #74016, #51460 ) ;
#59125=CARTESIAN_POINT ( 'NONE',  ( 2.449999999999998845, 0.000000000000000000, -0.3851141460153411078 ) ) ;
#59241=ADVANCED_FACE ( 'NONE', ( #69271 ), #18137, .F. ) ;
#59297=CARTESIAN_POINT ( 'NONE',  ( -9.974659986866640793E-15, -5.773502691896262640, -5.553418012614792509 ) ) ;
#59387=ORIENTED_EDGE ( 'NONE', *, *, #39901, .T. ) ;
#59425=CARTESIAN_POINT ( 'NONE',  ( 4.999999999999999112, -2.417244626924488049, -5.688952927922135139 ) ) ;
#59642=ORIENTED_EDGE ( 'NONE', *, *, #36187, .F. ) ;
#59692=CARTESIAN_POINT ( 'NONE',  ( 0.000000000000000000, 0.000000000000000000, -0.3501037691048548561 ) ) ;
#59728=LINE ( 'NONE', #43191, #20100 ) ;
#59767=DIRECTION ( 'NONE',  ( 1.000000000000000000, 0.000000000000000000, 0.000000000000000000 ) ) ;
#59773=EDGE_CURVE ( 'NONE', #38512, #40400, #29658, .T. ) ;
#59780=SURFACE_STYLE_FILL_AREA ( #36831 ) ;
#59893=CARTESIAN_POINT ( 'NONE',  ( -4.088737910769898676, 3.412868758467427988, -1.160540885688320589 ) ) ;
#60052=CARTESIAN_POINT ( 'NONE',  ( 0.000000000000000000, 0.000000000000000000, -5.974599999999999689 ) ) ;
#60058=CARTESIAN_POINT ( 'NONE',  ( 0.4079457818577056916, -5.537975084925947478, -5.689399939901065295 ) ) ;
#60431=CARTESIAN_POINT ( 'NONE',  ( 0.000000000000000000, 5.773502691896262640, -6.000000000000000000 ) ) ;
#60732=ORIENTED_EDGE ( 'NONE', *, *, #41254, .T. ) ;
#60797=DIRECTION ( 'NONE',  ( -1.000000000000000000, 0.000000000000000000, 0.000000000000000000 ) ) ;
#60805=DIRECTION ( 'NONE',  ( 0.000000000000000000, 0.000000000000000000, -1.000000000000000000 ) ) ;
#60808=CARTESIAN_POINT ( 'NONE',  ( -2.500000000000003997, -4.330127018922192761, -6.000000000000000000 ) ) ;
#60838=EDGE_CURVE ( 'NONE', #70907, #69466, #42942, .T. ) ;
#60943=CARTESIAN_POINT ( 'NONE',  ( -3.346878500200759277, -3.841181488860386573, -5.948595712916170619 ) ) ;
#60959=CARTESIAN_POINT ( 'NONE',  ( 2.744988726042924210, -4.188682711992893992, -0.5083873451168847701 ) ) ;
#61217=ADVANCED_FACE ( 'NONE', ( #66163 ), #31983, .T. ) ;
#61295=ORIENTED_EDGE ( 'NONE', *, *, #34105, .F. ) ;
#61478=ORIENTED_EDGE ( 'NONE', *, *, #19446, .T. ) ;
#61645=CIRCLE ( 'NONE', #2857, 4.749999999999999112 ) ;
#61796=ADVANCED_FACE ( 'NONE', ( #4787, #55891 ), #54779, .T. ) ;
#61813=ORIENTED_EDGE ( 'NONE', *, *, #15121, .T. ) ;
#61838=CARTESIAN_POINT ( 'NONE',  ( -3.000000000000000000, 0.000000000000000000, -5.974599999999999689 ) ) ;
#61864=CARTESIAN_POINT ( 'NONE',  ( 0.000000000000000000, 0.000000000000000000, -0.3851141460153411078 ) ) ;
#61874=SURFACE_STYLE_USAGE ( .BOTH. , #55484 ) ;
#61911=DIRECTION ( 'NONE',  ( 0.000000000000000000, 0.000000000000000000, -1.000000000000000000 ) ) ;
#62176=DIRECTION ( 'NONE',  ( 1.000000000000000000, 0.000000000000000000, 0.000000000000000000 ) ) ;
#62345=FACE_OUTER_BOUND ( 'NONE', #36413, .T. ) ;
#62489=CARTESIAN_POINT ( 'NONE',  ( -2.500000000000003997, 4.330127018922192761, -6.000000000000000000 ) ) ;
#62562=DIRECTION ( 'NONE',  ( -0.000000000000000000, -0.000000000000000000, 1.000000000000000000 ) ) ;
#62655=DIRECTION ( 'NONE',  ( -0.000000000000000000, -0.000000000000000000, 1.000000000000000000 ) ) ;
#62794=CARTESIAN_POINT ( 'NONE',  ( 2.500000000000000000, 0.000000000000000000, -0.3501037691048548561 ) ) ;
#62841=AXIS2_PLACEMENT_3D ( 'NONE', #44575, #5476, #55844 ) ;
#62875=AXIS2_PLACEMENT_3D ( 'NONE', #47665, #70211, #52943 ) ;
#63139=CARTESIAN_POINT ( 'NONE',  ( -4.999999999999999112, 2.691270400161067666, -1.881368198414903548 ) ) ;
#63141=CARTESIAN_POINT ( 'NONE',  ( 2.981146944884248473, 4.052336700773506273, -0.5666985376598466795 ) ) ;
#63143=DIRECTION ( 'NONE',  ( -1.000000000000000000, 0.000000000000000000, 0.000000000000000000 ) ) ;
#63208=CARTESIAN_POINT ( 'NONE',  ( 0.000000000000000000, 0.000000000000000000, -6.000000000000000000 ) ) ;
#63225=DIRECTION ( 'NONE',  ( -1.000000000000000000, 0.000000000000000000, 0.000000000000000000 ) ) ;
#63503=CARTESIAN_POINT ( 'NONE',  ( 4.084562121000262280, 3.415279651815005924, -1.156968425231149844 ) ) ;
#63662=B_SPLINE_CURVE_WITH_KNOTS ( 'NONE', 3,
 ( #7347, #46833, #6959, #29884 ),
 .UNSPECIFIED., .F., .F.,
 ( 4, 4 ),
 ( 2.380735200821679637E-07, 0.002921158011986721599 ),
 .UNSPECIFIED. ) ;
#63698=CARTESIAN_POINT ( 'NONE',  ( 4.749999999999999112, 5.817072295949926440E-16, 0.000000000000000000 ) ) ;
#63723=ORIENTED_EDGE ( 'NONE', *, *, #33329, .T. ) ;
#63756=B_SPLINE_CURVE_WITH_KNOTS ( 'NONE', 3,
 ( #50664, #57805, #28470, #16844, #40138, #39777, #23228, #51405 ),
 .UNSPECIFIED., .F., .F.,
 ( 4, 2, 2, 4 ),
 ( 0.002921158011986721599, 0.003648658599403073119, 0.004376159186819424639, 0.005831160361652126811 ),
 .UNSPECIFIED. ) ;
#63760=CARTESIAN_POINT ( 'NONE',  ( -2.287832656137188891, 4.452621892014637872, -6.000000000000004441 ) ) ;
#63768=CARTESIAN_POINT ( 'NONE',  ( -0.1709976663249050954, -5.674777143212785369, -1.879366290983713217 ) ) ;
#63797=ORIENTED_EDGE ( 'NONE', *, *, #25310, .T. ) ;
#64334=CARTESIAN_POINT ( 'NONE',  ( 5.000000000000000000, -0.9724665692850895660, -5.958069561147902427 ) ) ;
#64381=CARTESIAN_POINT ( 'NONE',  ( 2.500000000000000000, 0.000000000000000000, -5.624496230895140947 ) ) ;
#64433=VECTOR ( 'NONE', #44214, 1000.000000000000000 ) ;
#64498=DIRECTION ( 'NONE',  ( 0.8660254037844382635, 0.5000000000000005551, 0.000000000000000000 ) ) ;
#64529=CIRCLE ( 'NONE', #38067, 2.500000000000000000 ) ;
#64572=CARTESIAN_POINT ( 'NONE',  ( 5.000000000000000888, 0.000000000000000000, -6.000000000000000000 ) ) ;
#64661=EDGE_LOOP ( 'NONE', ( #5212, #38825, #3458, #24615 ) ) ;
#64753=CARTESIAN_POINT ( 'NONE',  ( 0.000000000000000000, 0.000000000000000000, -6.000000000000001776 ) ) ;
#64755=EDGE_CURVE ( 'NONE', #36601, #18028, #14275, .T. ) ;
#64757=ORIENTED_EDGE ( 'NONE', *, *, #70883, .F. ) ;
#64771=LINE ( 'NONE', #23798, #96 ) ;
#64922=B_SPLINE_CURVE_WITH_KNOTS ( 'NONE', 3,
 ( #35905, #63768, #35537, #46838, #69754, #35175, #23899, #6968, #29889, #52092, #11496, #12239, #58473, #6608, #74286, #52455, #40081, #23525, #12606, #24274 ),
 .UNSPECIFIED., .F., .F.,
 ( 4, 2, 2, 2, 2, 2, 2, 2, 2, 4 ),
 ( 2.781148923622390442E-07, 0.0008372784139766601373, 0.001674278713060957900, 0.002511279012145256097, 0.003348279311229553860, 0.003766779460771703825, 0.004185279610313853357, 0.005022279909398152421, 0.005859280208482451485, 0.006696280507566749682 ),
 .UNSPECIFIED. ) ;
#65341=FACE_OUTER_BOUND ( 'NONE', #42304, .T. ) ;
#65367=DIRECTION ( 'NONE',  ( -0.5000000000000006661, -0.8660254037844382635, 0.000000000000000000 ) ) ;
#65403=EDGE_LOOP ( 'NONE', ( #35166, #22648, #18786 ) ) ;
#65494=CARTESIAN_POINT ( 'NONE',  ( -3.000000000000000000, 3.673940397442059868E-16, -6.000000000000001776 ) ) ;
#65530=CARTESIAN_POINT ( 'NONE',  ( -4.829002333675109782, 2.985476894631601485, -1.879366290983708110 ) ) ;
#65734=ORIENTED_EDGE ( 'NONE', *, *, #56301, .F. ) ;
#65774=VERTEX_POINT ( 'NONE', #2574 ) ;
#65935=ORIENTED_EDGE ( 'NONE', *, *, #41679, .F. ) ;
#66121=CARTESIAN_POINT ( 'NONE',  ( 0.000000000000000000, 0.000000000000000000, 0.000000000000000000 ) ) ;
#66163=FACE_OUTER_BOUND ( 'NONE', #65403, .T. ) ;
#66298=EDGE_LOOP ( 'NONE', ( #60732, #16161, #71683 ) ) ;
#66364=CARTESIAN_POINT ( 'NONE',  ( 0.000000000000000000, 0.000000000000000000, -6.000000000000001776 ) ) ;
#67038=PRODUCT_CONTEXT ( 'NONE', #34457, 'mechanical' ) ;
#67131=SHAPE_REPRESENTATION_RELATIONSHIP ( 'NONE' , 'NONE' ,  #23018, #74006 ) ;
#67208=CARTESIAN_POINT ( 'NONE',  ( -5.000000000000000000, -2.886751345948134428, -2.080000000000000071 ) ) ;
#67322=ORIENTED_EDGE ( 'NONE', *, *, #52822, .F. ) ;
#67342=CARTESIAN_POINT ( 'NONE',  ( 4.829002333675111558, -2.985476894631607259, -1.879366290983715881 ) ) ;
#67507=FILL_AREA_STYLE_COLOUR ( '', #9936 ) ;
#67546=AXIS2_PLACEMENT_3D ( 'NONE', #49774, #53396, #11056 ) ;
#67733=FACE_OUTER_BOUND ( 'NONE', #4723, .T. ) ;
#67879=FILL_AREA_STYLE ('',( #67507 ) ) ;
#68121=CONICAL_SURFACE ( 'NONE', #9294, 5.000000000000000888, 1.047197551196596299 ) ;
#68124=CIRCLE ( 'NONE', #51316, 5.000000000000000888 ) ;
#68205=AXIS2_PLACEMENT_3D ( 'NONE', #61864, #22377, #29388 ) ;
#68285=ORIENTED_EDGE ( 'NONE', *, *, #24271, .F. ) ;
#68345=VERTEX_POINT ( 'NONE', #34177 ) ;
#68398=CARTESIAN_POINT ( 'NONE',  ( -4.999999999999999112, 0.2838785441256745923, -0.5080592402122393603 ) ) ;
#68400=CARTESIAN_POINT ( 'NONE',  ( 1.546821644788039851, 4.880444798889544522, -0.7375898304884582757 ) ) ;
#68433=EDGE_LOOP ( 'NONE', ( #3088, #26396, #1103, #38376 ) ) ;
#68449=EDGE_CURVE ( 'NONE', #852, #40220, #49100, .T. ) ;
#68742=CARTESIAN_POINT ( 'NONE',  ( -5.000000000000000888, -1.936377641173862463, -5.802630826755077464 ) ) ;
#68769=CARTESIAN_POINT ( 'NONE',  ( 0.9112620892300974385, 5.247385279376962863, -1.160540885688332136 ) ) ;
#68821=CARTESIAN_POINT ( 'NONE',  ( -5.000000000000000000, -1.096207231254244352, -0.7463930790433302986 ) ) ;
#68925=CARTESIAN_POINT ( 'NONE',  ( -5.000000000000000888, 0.9828435001097632906, -5.956909652965543422 ) ) ;
#69084=CARTESIAN_POINT ( 'NONE',  ( 0.000000000000000000, 0.000000000000000000, -6.000000000000000000 ) ) ;
#69182=CARTESIAN_POINT ( 'NONE',  ( 5.000000000000000888, -1.831125658499874742, -1.158123955083391943 ) ) ;
#69271=FACE_OUTER_BOUND ( 'NONE', #68433, .T. ) ;
#69294=DIRECTION ( 'NONE',  ( 0.000000000000000000, 0.000000000000000000, 1.000000000000000000 ) ) ;
#69466=VERTEX_POINT ( 'NONE', #6536 ) ;
#69699=EDGE_CURVE ( 'NONE', #13774, #2617, #34908, .T. ) ;
#69754=CARTESIAN_POINT ( 'NONE',  ( -0.9112620892301054321, -5.247385279376963751, -1.160540885688338131 ) ) ;
#69926=FACE_OUTER_BOUND ( 'NONE', #1234, .T. ) ;
#69943=CIRCLE ( 'NONE', #67546, 5.000000000000000888 ) ;
#69945=CARTESIAN_POINT ( 'NONE',  ( -5.000000000000000000, 2.886751345948137981, -5.553418012614792509 ) ) ;
#69979=CARTESIAN_POINT ( 'NONE',  ( 5.000000000000002665, -2.886751345948134873, -5.553418012614792509 ) ) ;
#70105=CARTESIAN_POINT ( 'NONE',  ( 0.000000000000000000, 0.000000000000000000, -5.624496230895140947 ) ) ;
#70107=CARTESIAN_POINT ( 'NONE',  ( -0.8192951148925873284, 5.300482436767278926, -5.801655677627841179 ) ) ;
#70211=DIRECTION ( 'NONE',  ( 0.000000000000000000, 0.000000000000000000, 1.000000000000000000 ) ) ;
#70259=CARTESIAN_POINT ( 'NONE',  ( 5.000000000000000000, 6.074766241781102566E-16, -0.5080592402122449114 ) ) ;
#70512=EDGE_CURVE ( 'NONE', #55045, #55663, #1957, .T. ) ;
#70549=CARTESIAN_POINT ( 'NONE',  ( 0.8192951148925871063, -5.300482436767286920, -5.801655677627835850 ) ) ;
#70821=ORIENTED_EDGE ( 'NONE', *, *, #13487, .T. ) ;
#70883=EDGE_CURVE ( 'NONE', #36601, #46616, #39843, .T. ) ;
#70907=VERTEX_POINT ( 'NONE', #62794 ) ;
#70980=CARTESIAN_POINT ( 'NONE',  ( -5.000000000000000000, -2.886751345948133540, -6.000000000000000000 ) ) ;
#70988=DIRECTION ( 'NONE',  ( 1.000000000000000000, 0.000000000000000000, 0.000000000000000000 ) ) ;
#71120=B_SPLINE_CURVE_WITH_KNOTS ( 'NONE', 3,
 ( #22156, #45096, #74015, #28520, #68769, #45474, #68400, #51459, #16, #17257, #40192, #63141, #11594, #379, #40552, #63503, #41652, #25109, #19461, #25479 ),
 .UNSPECIFIED., .F., .F.,
 ( 4, 2, 2, 2, 2, 2, 2, 2, 2, 4 ),
 ( 2.781148923614798380E-07, 0.0008372784139766645825, 0.001674278713060967658, 0.002511279012145270842, 0.003348279311229572942, 0.003766779460771723775, 0.004185279610313873307, 0.005022279909398174105, 0.005859280208482472302, 0.006696280507566771366 ),
 .UNSPECIFIED. ) ;
#71140=CARTESIAN_POINT ( 'NONE',  ( -5.000000000000000000, 2.886751345948126879, -2.079999999999992077 ) ) ;
#71190=DIRECTION ( 'NONE',  ( 0.000000000000000000, 0.000000000000000000, -1.000000000000000000 ) ) ;
#71232=DIRECTION ( 'NONE',  ( 0.000000000000000000, 0.000000000000000000, 1.000000000000000000 ) ) ;
#71603=DIRECTION ( 'NONE',  ( -1.000000000000000000, 0.000000000000000000, 0.000000000000000000 ) ) ;
#71683=ORIENTED_EDGE ( 'NONE', *, *, #34105, .T. ) ;
#71784=CARTESIAN_POINT ( 'NONE',  ( 4.182066831946704255, -3.358985280702828646, -5.826062401966622950 ) ) ;
#71928=ORIENTED_EDGE ( 'NONE', *, *, #485, .T. ) ;
#72051=ORIENTED_EDGE ( 'NONE', *, *, #9273, .T. ) ;
#72374=CARTESIAN_POINT ( 'NONE',  ( -4.749999999999999112, 0.000000000000000000, 0.000000000000000000 ) ) ;
#72535=ORIENTED_EDGE ( 'NONE', *, *, #29206, .T. ) ;
#72588=CARTESIAN_POINT ( 'NONE',  ( 0.9154378789997317245, -5.244974386029391589, -1.156968425231173381 ) ) ;
#72802=EDGE_LOOP ( 'NONE', ( #3464, #11011, #59387, #64757 ) ) ;
#72888=CARTESIAN_POINT ( 'NONE',  ( 3.351853367131008454, -3.838309248099023296, -6.000000000000000000 ) ) ;
#73041=DIRECTION ( 'NONE',  ( 0.000000000000000000, 0.000000000000000000, -1.000000000000000000 ) ) ;
#73339=CARTESIAN_POINT ( 'NONE',  ( 4.088737910769899564, -3.412868758467433317, -1.160540885688329249 ) ) ;
#73364=CARTESIAN_POINT ( 'NONE',  ( -0.1714266706912549731, 5.674529457426383594, -1.878862934774786275 ) ) ;
#73586=ORIENTED_EDGE ( 'NONE', *, *, #2017, .T. ) ;
#73765=EDGE_LOOP ( 'NONE', ( #43929, #42357, #61813, #41496 ) ) ;
#73824=AXIS2_PLACEMENT_3D ( 'NONE', #24622, #24264, #1735 ) ;
#73899=DIRECTION ( 'NONE',  ( 1.000000000000000000, 0.000000000000000000, 0.000000000000000000 ) ) ;
#73952=CARTESIAN_POINT ( 'NONE',  ( -4.749999999999999112, 0.000000000000000000, 0.000000000000000000 ) ) ;
#73987=CARTESIAN_POINT ( 'NONE',  ( -5.000000000000000000, -2.886751345948137981, -5.553418012614792509 ) ) ;
#74006=ADVANCED_BREP_SHAPE_REPRESENTATION ( '', ( #11785, #43395 ), #47140 ) ;
#74015=CARTESIAN_POINT ( 'NONE',  ( 0.3476802294499899415, 5.572769417831398897, -1.687189089856316215 ) ) ;
#74016=DIRECTION ( 'NONE',  ( 0.000000000000000000, -0.000000000000000000, 1.000000000000000000 ) ) ;
#74019=AXIS2_PLACEMENT_3D ( 'NONE', #37217, #30438, #2296 ) ;
#74249=( NAMED_UNIT ( * ) SI_UNIT ( $, .STERADIAN. ) SOLID_ANGLE_UNIT ( ) );
#74286=CARTESIAN_POINT ( 'NONE',  ( -3.667169054266697259, -3.656261651251520917, -0.8603634151101461347 ) ) ;
ENDSEC;
END-ISO-10303-21;
